ISO-10303-21;
HEADER;
/* Generated by software containing ST-Developer
 * from STEP Tools, Inc. (www.steptools.com) 
 */
/* OPTION: using custom renumber hook */

FILE_DESCRIPTION(
/* description */ ('STEP AP242 Edition 2', 'CAx-IF Rec.Pracs.---Representation and Presentation of Product Manufa
cturing Information (PMI)---4.0---2014-10-13', 'CAx-IF Rec.Pracs.---3D Tessellated Geometry---0.4---2014-09-14', '2;1', 'CAx-IF Rec.Pracs.---User Defined Attributes---1.5---2016-08-15'),
/* implementation_level */ '2;1');

FILE_NAME(
/* name */ 'floating_ring_bottom_connector.step',
/* time_stamp */ '2026-10-08T12:15:07Z',
/* author */ (''),
/* organization */ (''),
/* preprocessor_version */ 'ST-DEVELOPER v20',
/* originating_system */ 'ONSHAPE BY PTC INC, 1.221',
/* authorisation */ '  ');

FILE_SCHEMA (('AP242_MANAGED_MODEL_BASED_3D_ENGINEERING_MIM_LF { 1 0 10303 442 3 1 4 }'));
ENDSEC;

DATA;
#53=B_SPLINE_SURFACE_WITH_KNOTS('',3,3,((#31219,#31220,#31221,#31222,#31223,
#31224,#31225,#31226,#31227,#31228,#31229,#31230,#31231,#31232,#31233,#31234,
#31235,#31236,#31237,#31238,#31239,#31240,#31241,#31242,#31243,#31244,#31245,
#31246,#31247,#31248,#31249,#31250,#31251,#31252,#31253,#31254,#31255,#31256,
#31257,#31258,#31259,#31260,#31261,#31262,#31263,#31264,#31265,#31266,#31267,
#31268,#31269,#31270,#31271,#31272,#31273,#31274,#31275,#31276),(#31277,
#31278,#31279,#31280,#31281,#31282,#31283,#31284,#31285,#31286,#31287,#31288,
#31289,#31290,#31291,#31292,#31293,#31294,#31295,#31296,#31297,#31298,#31299,
#31300,#31301,#31302,#31303,#31304,#31305,#31306,#31307,#31308,#31309,#31310,
#31311,#31312,#31313,#31314,#31315,#31316,#31317,#31318,#31319,#31320,#31321,
#31322,#31323,#31324,#31325,#31326,#31327,#31328,#31329,#31330,#31331,#31332,
#31333,#31334),(#31335,#31336,#31337,#31338,#31339,#31340,#31341,#31342,
#31343,#31344,#31345,#31346,#31347,#31348,#31349,#31350,#31351,#31352,#31353,
#31354,#31355,#31356,#31357,#31358,#31359,#31360,#31361,#31362,#31363,#31364,
#31365,#31366,#31367,#31368,#31369,#31370,#31371,#31372,#31373,#31374,#31375,
#31376,#31377,#31378,#31379,#31380,#31381,#31382,#31383,#31384,#31385,#31386,
#31387,#31388,#31389,#31390,#31391,#31392),(#31393,#31394,#31395,#31396,
#31397,#31398,#31399,#31400,#31401,#31402,#31403,#31404,#31405,#31406,#31407,
#31408,#31409,#31410,#31411,#31412,#31413,#31414,#31415,#31416,#31417,#31418,
#31419,#31420,#31421,#31422,#31423,#31424,#31425,#31426,#31427,#31428,#31429,
#31430,#31431,#31432,#31433,#31434,#31435,#31436,#31437,#31438,#31439,#31440,
#31441,#31442,#31443,#31444,#31445,#31446,#31447,#31448,#31449,#31450)),
 .UNSPECIFIED.,.F.,.F.,.F.,(4,4),(4,2,2,2,2,2,2,2,2,2,2,2,2,2,2,2,2,2,2,
2,2,2,2,2,2,2,2,2,4),(0.,1.),(0.,0.0259911760203312,0.0519823520406625,
0.0779735280609937,0.103964704081325,0.129955880101656,0.155947056121987,
0.181938232142319,0.20792940816265,0.233920584182981,0.259911760203312,
0.285902936223644,0.311894112243975,0.337885288264306,0.363876464284637,
0.389867640304969,0.4158588163253,0.441849992345631,0.467841168365962,0.493832344386293,
0.519823520406625,0.571805872447287,0.62378822448795,0.675770576528612,
0.727752928569275,0.779735280609937,0.805726456630268,0.818722044640434,
0.8317176326506),.UNSPECIFIED.);
#60=COLOUR_RGB('', 0.66274510, 0.83137255, 0.94901961);
#206=SHAPE_REPRESENTATION_RELATIONSHIP('','',#13780,#233);
#233=ADVANCED_BREP_SHAPE_REPRESENTATION('',(#13724),#45470);
#271=TOROIDAL_SURFACE('',#14011,0.0115,0.001);
#272=TOROIDAL_SURFACE('',#14015,0.002,0.001);
#273=TOROIDAL_SURFACE('',#14019,0.002,0.001);
#274=TOROIDAL_SURFACE('',#14029,0.002,0.001);
#275=TOROIDAL_SURFACE('',#14033,0.002,0.001);
#276=TOROIDAL_SURFACE('',#14038,0.002,0.001);
#277=TOROIDAL_SURFACE('',#14042,0.002,0.001);
#278=TOROIDAL_SURFACE('',#14051,0.0065,0.001);
#279=TOROIDAL_SURFACE('',#14059,0.0115,0.001);
#280=TOROIDAL_SURFACE('',#14062,0.002,0.001);
#281=TOROIDAL_SURFACE('',#14066,0.002,0.001);
#282=TOROIDAL_SURFACE('',#14070,0.002,0.001);
#283=TOROIDAL_SURFACE('',#14074,0.002,0.001);
#284=TOROIDAL_SURFACE('',#14081,0.0115,0.001);
#285=TOROIDAL_SURFACE('',#14089,0.0065,0.001);
#286=TOROIDAL_SURFACE('',#14093,0.002,0.001);
#287=TOROIDAL_SURFACE('',#14096,0.002,0.001);
#288=TOROIDAL_SURFACE('',#14100,0.002,0.001);
#289=TOROIDAL_SURFACE('',#14104,0.002,0.001);
#290=TOROIDAL_SURFACE('',#14107,0.0115,0.001);
#291=TOROIDAL_SURFACE('',#14115,0.0115,0.001);
#292=TOROIDAL_SURFACE('',#14123,0.002,0.001);
#293=TOROIDAL_SURFACE('',#14126,0.002,0.001);
#294=TOROIDAL_SURFACE('',#14130,0.002,0.001);
#295=TOROIDAL_SURFACE('',#14134,0.002,0.001);
#296=TOROIDAL_SURFACE('',#14141,0.0065,0.001);
#297=TOROIDAL_SURFACE('',#14149,0.0115,0.001);
#298=TOROIDAL_SURFACE('',#14153,0.002,0.001);
#299=TOROIDAL_SURFACE('',#14156,0.002,0.001);
#300=TOROIDAL_SURFACE('',#14159,0.002,0.001);
#301=TOROIDAL_SURFACE('',#14162,0.0065,0.001);
#302=TOROIDAL_SURFACE('',#14170,0.002,0.001);
#303=TOROIDAL_SURFACE('',#14220,0.0065,0.001);
#304=TOROIDAL_SURFACE('',#14221,0.0065,0.001);
#305=TOROIDAL_SURFACE('',#14222,0.01055,0.001);
#306=TOROIDAL_SURFACE('',#14224,0.00855,0.001);
#440=CIRCLE('',#14010,0.001);
#441=CIRCLE('',#14012,0.001);
#442=CIRCLE('',#14013,0.0125);
#443=CIRCLE('',#14014,0.0115);
#444=CIRCLE('',#14016,0.001);
#445=CIRCLE('',#14017,0.002);
#446=CIRCLE('',#14018,0.001);
#447=CIRCLE('',#14020,0.001);
#448=CIRCLE('',#14021,0.001);
#449=CIRCLE('',#14022,0.002);
#450=CIRCLE('',#14024,0.001);
#451=CIRCLE('',#14026,0.001);
#452=CIRCLE('',#14028,0.001);
#453=CIRCLE('',#14030,0.002);
#454=CIRCLE('',#14031,0.001);
#455=CIRCLE('',#14032,0.001);
#456=CIRCLE('',#14034,0.001);
#457=CIRCLE('',#14035,0.002);
#458=CIRCLE('',#14036,0.001);
#459=CIRCLE('',#14037,0.001);
#460=CIRCLE('',#14039,0.001);
#461=CIRCLE('',#14040,0.001);
#462=CIRCLE('',#14041,0.002);
#463=CIRCLE('',#14043,0.002);
#464=CIRCLE('',#14044,0.001);
#465=CIRCLE('',#14045,0.001);
#466=CIRCLE('',#14048,0.001);
#467=CIRCLE('',#14050,0.001);
#468=CIRCLE('',#14052,0.001);
#469=CIRCLE('',#14053,0.0075);
#470=CIRCLE('',#14054,0.0065);
#471=CIRCLE('',#14056,0.001);
#472=CIRCLE('',#14058,0.001);
#473=CIRCLE('',#14060,0.0115);
#474=CIRCLE('',#14061,0.0125);
#475=CIRCLE('',#14063,0.002);
#476=CIRCLE('',#14064,0.001);
#477=CIRCLE('',#14065,0.001);
#478=CIRCLE('',#14067,0.001);
#479=CIRCLE('',#14068,0.002);
#480=CIRCLE('',#14069,0.001);
#481=CIRCLE('',#14071,0.001);
#482=CIRCLE('',#14072,0.001);
#483=CIRCLE('',#14073,0.002);
#484=CIRCLE('',#14075,0.001);
#485=CIRCLE('',#14076,0.002);
#486=CIRCLE('',#14078,0.001);
#487=CIRCLE('',#14080,0.001);
#488=CIRCLE('',#14082,0.001);
#489=CIRCLE('',#14083,0.0115);
#490=CIRCLE('',#14084,0.0125);
#491=CIRCLE('',#14086,0.001);
#492=CIRCLE('',#14088,0.001);
#493=CIRCLE('',#14090,0.001);
#494=CIRCLE('',#14091,0.0065);
#495=CIRCLE('',#14092,0.0075);
#496=CIRCLE('',#14094,0.002);
#497=CIRCLE('',#14095,0.001);
#498=CIRCLE('',#14097,0.001);
#499=CIRCLE('',#14098,0.002);
#500=CIRCLE('',#14099,0.001);
#501=CIRCLE('',#14101,0.001);
#502=CIRCLE('',#14102,0.001);
#503=CIRCLE('',#14103,0.002);
#504=CIRCLE('',#14105,0.001);
#505=CIRCLE('',#14106,0.002);
#506=CIRCLE('',#14108,0.001);
#507=CIRCLE('',#14109,0.0125);
#508=CIRCLE('',#14110,0.0115);
#509=CIRCLE('',#14112,0.001);
#510=CIRCLE('',#14114,0.001);
#511=CIRCLE('',#14116,0.001);
#512=CIRCLE('',#14117,0.0125);
#513=CIRCLE('',#14118,0.0115);
#514=CIRCLE('',#14120,0.001);
#515=CIRCLE('',#14122,0.001);
#516=CIRCLE('',#14124,0.002);
#517=CIRCLE('',#14125,0.001);
#518=CIRCLE('',#14127,0.001);
#519=CIRCLE('',#14128,0.002);
#520=CIRCLE('',#14129,0.001);
#521=CIRCLE('',#14131,0.001);
#522=CIRCLE('',#14132,0.001);
#523=CIRCLE('',#14133,0.002);
#524=CIRCLE('',#14135,0.001);
#525=CIRCLE('',#14136,0.002);
#526=CIRCLE('',#14138,0.001);
#527=CIRCLE('',#14140,0.001);
#528=CIRCLE('',#14142,0.001);
#529=CIRCLE('',#14143,0.0065);
#530=CIRCLE('',#14144,0.0075);
#531=CIRCLE('',#14146,0.001);
#532=CIRCLE('',#14148,0.001);
#533=CIRCLE('',#14150,0.001);
#534=CIRCLE('',#14151,0.0115);
#535=CIRCLE('',#14152,0.0125);
#536=CIRCLE('',#14154,0.002);
#537=CIRCLE('',#14155,0.001);
#538=CIRCLE('',#14157,0.001);
#539=CIRCLE('',#14158,0.002);
#540=CIRCLE('',#14160,0.001);
#541=CIRCLE('',#14161,0.002);
#542=CIRCLE('',#14163,0.001);
#543=CIRCLE('',#14164,0.0075);
#544=CIRCLE('',#14165,0.0065);
#545=CIRCLE('',#14167,0.001);
#546=CIRCLE('',#14169,0.001);
#547=CIRCLE('',#14171,0.002);
#548=CIRCLE('',#14173,0.00277876);
#549=CIRCLE('',#14174,0.0012192);
#550=CIRCLE('',#14176,0.00277876);
#551=CIRCLE('',#14177,0.0012192);
#552=CIRCLE('',#14179,0.00277876);
#553=CIRCLE('',#14180,0.0012192);
#554=CIRCLE('',#14185,0.00655);
#555=CIRCLE('',#14186,0.00855);
#556=CIRCLE('',#14188,0.00277876);
#557=CIRCLE('',#14189,0.00277876);
#558=CIRCLE('',#14190,0.00277876);
#559=CIRCLE('',#14191,0.0065);
#560=CIRCLE('',#14192,0.01055);
#561=CIRCLE('',#14196,0.0075);
#562=CIRCLE('',#14197,0.0075);
#563=CIRCLE('',#14207,0.0065);
#564=CIRCLE('',#14208,0.0012192);
#565=CIRCLE('',#14209,0.0012192);
#566=CIRCLE('',#14210,0.0012192);
#567=CIRCLE('',#14211,0.00655);
#568=CIRCLE('',#14223,0.00955);
#1098=B_SPLINE_CURVE_WITH_KNOTS('',3,(#30747,#30748,#30749,#30750,#30751),
 .UNSPECIFIED.,.F.,.F.,(4,1,4),(0.,0.000813104509733637,0.00162620901946727),
 .UNSPECIFIED.);
#1099=B_SPLINE_CURVE_WITH_KNOTS('',3,(#30818,#30819,#30820,#30821,#30822),
 .UNSPECIFIED.,.F.,.F.,(4,1,4),(0.,0.000813104509733632,0.00162620901946726),
 .UNSPECIFIED.);
#1242=PLANE('',#14172);
#1243=PLANE('',#14175);
#1244=PLANE('',#14178);
#1245=PLANE('',#14182);
#1246=PLANE('',#14183);
#1247=PLANE('',#14184);
#1248=PLANE('',#14187);
#1249=PLANE('',#14194);
#1250=PLANE('',#14198);
#1251=PLANE('',#14200);
#1252=PLANE('',#14201);
#1253=PLANE('',#14203);
#1254=PLANE('',#14205);
#1255=PLANE('',#14206);
#1578=CYLINDRICAL_SURFACE('',#14009,0.001);
#1579=CYLINDRICAL_SURFACE('',#14023,0.001);
#1580=CYLINDRICAL_SURFACE('',#14025,0.001);
#1581=CYLINDRICAL_SURFACE('',#14027,0.001);
#1582=CYLINDRICAL_SURFACE('',#14046,0.001);
#1583=CYLINDRICAL_SURFACE('',#14047,0.001);
#1584=CYLINDRICAL_SURFACE('',#14049,0.001);
#1585=CYLINDRICAL_SURFACE('',#14055,0.001);
#1586=CYLINDRICAL_SURFACE('',#14057,0.001);
#1587=CYLINDRICAL_SURFACE('',#14077,0.001);
#1588=CYLINDRICAL_SURFACE('',#14079,0.001);
#1589=CYLINDRICAL_SURFACE('',#14085,0.001);
#1590=CYLINDRICAL_SURFACE('',#14087,0.001);
#1591=CYLINDRICAL_SURFACE('',#14111,0.001);
#1592=CYLINDRICAL_SURFACE('',#14113,0.001);
#1593=CYLINDRICAL_SURFACE('',#14119,0.001);
#1594=CYLINDRICAL_SURFACE('',#14121,0.001);
#1595=CYLINDRICAL_SURFACE('',#14137,0.001);
#1596=CYLINDRICAL_SURFACE('',#14139,0.001);
#1597=CYLINDRICAL_SURFACE('',#14145,0.001);
#1598=CYLINDRICAL_SURFACE('',#14147,0.001);
#1599=CYLINDRICAL_SURFACE('',#14166,0.001);
#1600=CYLINDRICAL_SURFACE('',#14168,0.001);
#1601=CYLINDRICAL_SURFACE('',#14181,0.00753201094464286);
#1602=CYLINDRICAL_SURFACE('',#14193,0.0125);
#1603=CYLINDRICAL_SURFACE('',#14195,0.0075);
#1604=CYLINDRICAL_SURFACE('',#14199,0.0125);
#1605=CYLINDRICAL_SURFACE('',#14202,0.0125);
#1606=CYLINDRICAL_SURFACE('',#14204,0.0075);
#1607=CYLINDRICAL_SURFACE('',#14212,0.00655);
#1608=CYLINDRICAL_SURFACE('',#14213,0.0075);
#1609=CYLINDRICAL_SURFACE('',#14214,0.0012192);
#1610=CYLINDRICAL_SURFACE('',#14215,0.00277876);
#1611=CYLINDRICAL_SURFACE('',#14216,0.0012192);
#1612=CYLINDRICAL_SURFACE('',#14217,0.00277876);
#1613=CYLINDRICAL_SURFACE('',#14218,0.0012192);
#1614=CYLINDRICAL_SURFACE('',#14219,0.00277876);
#1866=(
BOUNDED_CURVE()
B_SPLINE_CURVE(2,(#31140,#31141,#31142,#31143,#31144,#31145,#31146,#31147,
#31148,#31149,#31150),.UNSPECIFIED.,.F.,.F.)
B_SPLINE_CURVE_WITH_KNOTS((3,2,2,2,2,3),(0.,0.05,0.1,0.15,0.2,0.25),
 .UNSPECIFIED.)
CURVE()
GEOMETRIC_REPRESENTATION_ITEM()
RATIONAL_B_SPLINE_CURVE((1.,0.951056516295154,1.,0.951056516295154,1.,0.951056516295154,
1.,0.951056516295154,1.,0.951056516295154,1.))
REPRESENTATION_ITEM('')
);
#1867=(
BOUNDED_CURVE()
B_SPLINE_CURVE(2,(#31152,#31153,#31154,#31155,#31156,#31157,#31158,#31159,
#31160,#31161,#31162),.UNSPECIFIED.,.F.,.F.)
B_SPLINE_CURVE_WITH_KNOTS((3,2,2,2,2,3),(0.25,0.3,0.35,0.4,0.45,0.5),
 .UNSPECIFIED.)
CURVE()
GEOMETRIC_REPRESENTATION_ITEM()
RATIONAL_B_SPLINE_CURVE((1.,0.951056516295153,1.,0.951056516295154,1.,0.951056516295154,
1.,0.951056516295154,1.,0.951056516295154,1.))
REPRESENTATION_ITEM('')
);
#1868=(
BOUNDED_CURVE()
B_SPLINE_CURVE(2,(#31164,#31165,#31166,#31167,#31168,#31169,#31170,#31171,
#31172,#31173,#31174),.UNSPECIFIED.,.F.,.F.)
B_SPLINE_CURVE_WITH_KNOTS((3,2,2,2,2,3),(0.5,0.55,0.6,0.65,0.7,0.75),
 .UNSPECIFIED.)
CURVE()
GEOMETRIC_REPRESENTATION_ITEM()
RATIONAL_B_SPLINE_CURVE((1.,0.951056516295153,1.,0.951056516295154,1.,0.951056516295154,
1.,0.951056516295154,1.,0.951056516295154,1.))
REPRESENTATION_ITEM('')
);
#1869=(
BOUNDED_CURVE()
B_SPLINE_CURVE(2,(#31176,#31177,#31178,#31179,#31180),.UNSPECIFIED.,.F.,
 .F.)
B_SPLINE_CURVE_WITH_KNOTS((3,2,3),(0.75,0.8,0.826757087433802),
 .UNSPECIFIED.)
CURVE()
GEOMETRIC_REPRESENTATION_ITEM()
RATIONAL_B_SPLINE_CURVE((1.,0.951056516295153,1.,0.973808298543891,0.975649142923828))
REPRESENTATION_ITEM('')
);
#1870=(
BOUNDED_CURVE()
B_SPLINE_CURVE(2,(#31184,#31185,#31186,#31187,#31188,#31189,#31190,#31191,
#31192,#31193,#31194,#31195,#31196,#31197,#31198,#31199,#31200,#31201,#31202,
#31203,#31204,#31205,#31206,#31207,#31208,#31209,#31210,#31211,#31212,#31213,
#31214,#31215,#31216,#31217,#31218),.UNSPECIFIED.,.F.,.F.)
B_SPLINE_CURVE_WITH_KNOTS((3,2,2,2,2,2,2,2,2,2,2,2,2,2,2,2,2,3),(0.,0.05,
0.1,0.15,0.2,0.25,0.3,0.35,0.4,0.45,0.5,0.55,0.6,0.65,0.7,0.75,0.8,0.826757087433802),
 .UNSPECIFIED.)
CURVE()
GEOMETRIC_REPRESENTATION_ITEM()
RATIONAL_B_SPLINE_CURVE((1.,0.951056516295154,1.,0.951056516295154,1.,0.951056516295154,
1.,0.951056516295154,1.,0.951056516295154,1.,0.951056516295154,1.,0.951056516295154,
1.,0.951056516295154,1.,0.951056516295154,1.,0.951056516295154,1.,0.951056516295154,
1.,0.951056516295154,1.,0.951056516295154,1.,0.951056516295154,1.,0.951056516295154,
1.,0.951056516295154,1.,0.973808298543891,0.975649142923828))
REPRESENTATION_ITEM('')
);
#1871=(
BOUNDED_CURVE()
B_SPLINE_CURVE(2,(#31454,#31455,#31456,#31457,#31458,#31459,#31460,#31461,
#31462,#31463,#31464,#31465,#31466,#31467,#31468,#31469,#31470,#31471,#31472,
#31473,#31474,#31475,#31476,#31477,#31478,#31479,#31480,#31481,#31482,#31483,
#31484,#31485,#31486,#31487,#31488),.UNSPECIFIED.,.F.,.F.)
B_SPLINE_CURVE_WITH_KNOTS((3,2,2,2,2,2,2,2,2,2,2,2,2,2,2,2,2,3),(0.,0.05,
0.1,0.15,0.2,0.25,0.3,0.35,0.4,0.45,0.5,0.55,0.6,0.65,0.7,0.75,0.8,0.826757073484189),
 .UNSPECIFIED.)
CURVE()
GEOMETRIC_REPRESENTATION_ITEM()
RATIONAL_B_SPLINE_CURVE((1.,0.951056516295154,1.,0.951056516295154,1.,0.951056516295154,
1.,0.951056516295154,1.,0.951056516295154,1.,0.951056516295154,1.,0.951056516295154,
1.,0.951056516295154,1.,0.951056516295154,1.,0.951056516295154,1.,0.951056516295154,
1.,0.951056516295154,1.,0.951056516295154,1.,0.951056516295154,1.,0.951056516295154,
1.,0.951056516295154,1.,0.973808312198744,0.975649141004414))
REPRESENTATION_ITEM('')
);
#1872=(
BOUNDED_CURVE()
B_SPLINE_CURVE(2,(#31492,#31493,#31494,#31495,#31496),.UNSPECIFIED.,.F.,
 .F.)
B_SPLINE_CURVE_WITH_KNOTS((3,2,3),(0.75,0.8,0.826757130829527),
 .UNSPECIFIED.)
CURVE()
GEOMETRIC_REPRESENTATION_ITEM()
RATIONAL_B_SPLINE_CURVE((1.,0.951056516295153,1.,0.973808256065132,0.975649148895013))
REPRESENTATION_ITEM('')
);
#1873=(
BOUNDED_CURVE()
B_SPLINE_CURVE(2,(#31498,#31499,#31500,#31501,#31502,#31503,#31504,#31505,
#31506,#31507,#31508),.UNSPECIFIED.,.F.,.F.)
B_SPLINE_CURVE_WITH_KNOTS((3,2,2,2,2,3),(0.5,0.55,0.6,0.65,0.7,0.75),
 .UNSPECIFIED.)
CURVE()
GEOMETRIC_REPRESENTATION_ITEM()
RATIONAL_B_SPLINE_CURVE((1.,0.951056516295153,1.,0.951056516295154,1.,0.951056516295154,
1.,0.951056516295154,1.,0.951056516295154,1.))
REPRESENTATION_ITEM('')
);
#1874=(
BOUNDED_CURVE()
B_SPLINE_CURVE(2,(#31510,#31511,#31512,#31513,#31514,#31515,#31516,#31517,
#31518,#31519,#31520),.UNSPECIFIED.,.F.,.F.)
B_SPLINE_CURVE_WITH_KNOTS((3,2,2,2,2,3),(0.25,0.3,0.35,0.4,0.45,0.5),
 .UNSPECIFIED.)
CURVE()
GEOMETRIC_REPRESENTATION_ITEM()
RATIONAL_B_SPLINE_CURVE((1.,0.951056516295153,1.,0.951056516295154,1.,0.951056516295154,
1.,0.951056516295154,1.,0.951056516295154,1.))
REPRESENTATION_ITEM('')
);
#1875=(
BOUNDED_CURVE()
B_SPLINE_CURVE(2,(#31522,#31523,#31524,#31525,#31526,#31527,#31528,#31529,
#31530,#31531,#31532),.UNSPECIFIED.,.F.,.F.)
B_SPLINE_CURVE_WITH_KNOTS((3,2,2,2,2,3),(0.,0.05,0.1,0.15,0.2,0.25),
 .UNSPECIFIED.)
CURVE()
GEOMETRIC_REPRESENTATION_ITEM()
RATIONAL_B_SPLINE_CURVE((1.,0.951056516295154,1.,0.951056516295154,1.,0.951056516295154,
1.,0.951056516295154,1.,0.951056516295154,1.))
REPRESENTATION_ITEM('')
);
#2420=ORIENTED_EDGE('',*,*,#5857,.T.);
#2421=ORIENTED_EDGE('',*,*,#5858,.F.);
#2422=ORIENTED_EDGE('',*,*,#5859,.T.);
#2423=ORIENTED_EDGE('',*,*,#5860,.F.);
#2424=ORIENTED_EDGE('',*,*,#5861,.T.);
#2425=ORIENTED_EDGE('',*,*,#5862,.F.);
#2426=ORIENTED_EDGE('',*,*,#5859,.F.);
#2427=ORIENTED_EDGE('',*,*,#5863,.F.);
#2428=ORIENTED_EDGE('',*,*,#5864,.T.);
#2429=ORIENTED_EDGE('',*,*,#5865,.T.);
#2430=ORIENTED_EDGE('',*,*,#5857,.F.);
#2431=ORIENTED_EDGE('',*,*,#5866,.T.);
#2432=ORIENTED_EDGE('',*,*,#5867,.T.);
#2433=ORIENTED_EDGE('',*,*,#5868,.T.);
#2434=ORIENTED_EDGE('',*,*,#5861,.F.);
#2435=ORIENTED_EDGE('',*,*,#5869,.T.);
#2436=ORIENTED_EDGE('',*,*,#5870,.T.);
#2437=ORIENTED_EDGE('',*,*,#5871,.F.);
#2438=ORIENTED_EDGE('',*,*,#5866,.F.);
#2439=ORIENTED_EDGE('',*,*,#5872,.F.);
#2440=ORIENTED_EDGE('',*,*,#5873,.T.);
#2441=ORIENTED_EDGE('',*,*,#5874,.F.);
#2442=ORIENTED_EDGE('',*,*,#5867,.F.);
#2443=ORIENTED_EDGE('',*,*,#5875,.F.);
#2444=ORIENTED_EDGE('',*,*,#5876,.T.);
#2445=ORIENTED_EDGE('',*,*,#5877,.F.);
#2446=ORIENTED_EDGE('',*,*,#5868,.F.);
#2447=ORIENTED_EDGE('',*,*,#5878,.F.);
#2448=ORIENTED_EDGE('',*,*,#5879,.T.);
#2449=ORIENTED_EDGE('',*,*,#5880,.T.);
#2450=ORIENTED_EDGE('',*,*,#5870,.F.);
#2451=ORIENTED_EDGE('',*,*,#5881,.T.);
#2452=ORIENTED_EDGE('',*,*,#5882,.T.);
#2453=ORIENTED_EDGE('',*,*,#5883,.T.);
#2454=ORIENTED_EDGE('',*,*,#5884,.F.);
#2455=ORIENTED_EDGE('',*,*,#5885,.T.);
#2456=ORIENTED_EDGE('',*,*,#5886,.T.);
#2457=ORIENTED_EDGE('',*,*,#5887,.T.);
#2458=ORIENTED_EDGE('',*,*,#5873,.F.);
#2459=ORIENTED_EDGE('',*,*,#5888,.T.);
#2460=ORIENTED_EDGE('',*,*,#5889,.T.);
#2461=ORIENTED_EDGE('',*,*,#5890,.T.);
#2462=ORIENTED_EDGE('',*,*,#5876,.F.);
#2463=ORIENTED_EDGE('',*,*,#5891,.T.);
#2464=ORIENTED_EDGE('',*,*,#5892,.T.);
#2465=ORIENTED_EDGE('',*,*,#5893,.F.);
#2466=ORIENTED_EDGE('',*,*,#5881,.F.);
#2467=ORIENTED_EDGE('',*,*,#5894,.F.);
#2468=ORIENTED_EDGE('',*,*,#5895,.T.);
#2469=ORIENTED_EDGE('',*,*,#5896,.F.);
#2470=ORIENTED_EDGE('',*,*,#5885,.F.);
#2471=ORIENTED_EDGE('',*,*,#5897,.F.);
#2472=ORIENTED_EDGE('',*,*,#5898,.T.);
#2473=ORIENTED_EDGE('',*,*,#5899,.F.);
#2474=ORIENTED_EDGE('',*,*,#5882,.F.);
#2475=ORIENTED_EDGE('',*,*,#5900,.F.);
#2476=ORIENTED_EDGE('',*,*,#5901,.T.);
#2477=ORIENTED_EDGE('',*,*,#5902,.F.);
#2478=ORIENTED_EDGE('',*,*,#5886,.F.);
#2479=ORIENTED_EDGE('',*,*,#5903,.F.);
#2480=ORIENTED_EDGE('',*,*,#5904,.T.);
#2481=ORIENTED_EDGE('',*,*,#5905,.F.);
#2482=ORIENTED_EDGE('',*,*,#5887,.F.);
#2483=ORIENTED_EDGE('',*,*,#5906,.F.);
#2484=ORIENTED_EDGE('',*,*,#5907,.T.);
#2485=ORIENTED_EDGE('',*,*,#5908,.F.);
#2486=ORIENTED_EDGE('',*,*,#5891,.F.);
#2487=ORIENTED_EDGE('',*,*,#5909,.F.);
#2488=ORIENTED_EDGE('',*,*,#5890,.F.);
#2489=ORIENTED_EDGE('',*,*,#5910,.F.);
#2490=ORIENTED_EDGE('',*,*,#5892,.F.);
#2491=ORIENTED_EDGE('',*,*,#5911,.F.);
#2492=ORIENTED_EDGE('',*,*,#5912,.T.);
#2493=ORIENTED_EDGE('',*,*,#5913,.T.);
#2494=ORIENTED_EDGE('',*,*,#5895,.F.);
#2495=ORIENTED_EDGE('',*,*,#5914,.F.);
#2496=ORIENTED_EDGE('',*,*,#5915,.T.);
#2497=ORIENTED_EDGE('',*,*,#5916,.T.);
#2498=ORIENTED_EDGE('',*,*,#5898,.F.);
#2499=ORIENTED_EDGE('',*,*,#5917,.T.);
#2500=ORIENTED_EDGE('',*,*,#5918,.T.);
#2501=ORIENTED_EDGE('',*,*,#5919,.T.);
#2502=ORIENTED_EDGE('',*,*,#5901,.F.);
#2503=ORIENTED_EDGE('',*,*,#5920,.T.);
#2504=ORIENTED_EDGE('',*,*,#5921,.T.);
#2505=ORIENTED_EDGE('',*,*,#5922,.T.);
#2506=ORIENTED_EDGE('',*,*,#5907,.F.);
#2507=ORIENTED_EDGE('',*,*,#5904,.F.);
#2508=ORIENTED_EDGE('',*,*,#5923,.T.);
#2509=ORIENTED_EDGE('',*,*,#5924,.F.);
#2510=ORIENTED_EDGE('',*,*,#5913,.F.);
#2511=ORIENTED_EDGE('',*,*,#5925,.F.);
#2512=ORIENTED_EDGE('',*,*,#5926,.T.);
#2513=ORIENTED_EDGE('',*,*,#5927,.F.);
#2514=ORIENTED_EDGE('',*,*,#5917,.F.);
#2515=ORIENTED_EDGE('',*,*,#5928,.F.);
#2516=ORIENTED_EDGE('',*,*,#5929,.T.);
#2517=ORIENTED_EDGE('',*,*,#5930,.F.);
#2518=ORIENTED_EDGE('',*,*,#5915,.F.);
#2519=ORIENTED_EDGE('',*,*,#5931,.F.);
#2520=ORIENTED_EDGE('',*,*,#5932,.T.);
#2521=ORIENTED_EDGE('',*,*,#5933,.F.);
#2522=ORIENTED_EDGE('',*,*,#5918,.F.);
#2523=ORIENTED_EDGE('',*,*,#5934,.F.);
#2524=ORIENTED_EDGE('',*,*,#5935,.T.);
#2525=ORIENTED_EDGE('',*,*,#5936,.F.);
#2526=ORIENTED_EDGE('',*,*,#5919,.F.);
#2527=ORIENTED_EDGE('',*,*,#5937,.F.);
#2528=ORIENTED_EDGE('',*,*,#5938,.T.);
#2529=ORIENTED_EDGE('',*,*,#5939,.F.);
#2530=ORIENTED_EDGE('',*,*,#5921,.F.);
#2531=ORIENTED_EDGE('',*,*,#5940,.F.);
#2532=ORIENTED_EDGE('',*,*,#5941,.T.);
#2533=ORIENTED_EDGE('',*,*,#5942,.T.);
#2534=ORIENTED_EDGE('',*,*,#5926,.F.);
#2535=ORIENTED_EDGE('',*,*,#5923,.F.);
#2536=ORIENTED_EDGE('',*,*,#5943,.T.);
#2537=ORIENTED_EDGE('',*,*,#5944,.T.);
#2538=ORIENTED_EDGE('',*,*,#5929,.F.);
#2539=ORIENTED_EDGE('',*,*,#5945,.T.);
#2540=ORIENTED_EDGE('',*,*,#5946,.T.);
#2541=ORIENTED_EDGE('',*,*,#5947,.T.);
#2542=ORIENTED_EDGE('',*,*,#5932,.F.);
#2543=ORIENTED_EDGE('',*,*,#5948,.T.);
#2544=ORIENTED_EDGE('',*,*,#5949,.T.);
#2545=ORIENTED_EDGE('',*,*,#5950,.T.);
#2546=ORIENTED_EDGE('',*,*,#5938,.F.);
#2547=ORIENTED_EDGE('',*,*,#5935,.F.);
#2548=ORIENTED_EDGE('',*,*,#5951,.T.);
#2549=ORIENTED_EDGE('',*,*,#5952,.F.);
#2550=ORIENTED_EDGE('',*,*,#5942,.F.);
#2551=ORIENTED_EDGE('',*,*,#5953,.F.);
#2552=ORIENTED_EDGE('',*,*,#5954,.T.);
#2553=ORIENTED_EDGE('',*,*,#5955,.F.);
#2554=ORIENTED_EDGE('',*,*,#5945,.F.);
#2555=ORIENTED_EDGE('',*,*,#5956,.F.);
#2556=ORIENTED_EDGE('',*,*,#5957,.T.);
#2557=ORIENTED_EDGE('',*,*,#5958,.F.);
#2558=ORIENTED_EDGE('',*,*,#5943,.F.);
#2559=ORIENTED_EDGE('',*,*,#5959,.F.);
#2560=ORIENTED_EDGE('',*,*,#5960,.T.);
#2561=ORIENTED_EDGE('',*,*,#5961,.F.);
#2562=ORIENTED_EDGE('',*,*,#5946,.F.);
#2563=ORIENTED_EDGE('',*,*,#5962,.F.);
#2564=ORIENTED_EDGE('',*,*,#5963,.T.);
#2565=ORIENTED_EDGE('',*,*,#5964,.F.);
#2566=ORIENTED_EDGE('',*,*,#5947,.F.);
#2567=ORIENTED_EDGE('',*,*,#5965,.F.);
#2568=ORIENTED_EDGE('',*,*,#5966,.T.);
#2569=ORIENTED_EDGE('',*,*,#5967,.F.);
#2570=ORIENTED_EDGE('',*,*,#5949,.F.);
#2571=ORIENTED_EDGE('',*,*,#5968,.F.);
#2572=ORIENTED_EDGE('',*,*,#5969,.T.);
#2573=ORIENTED_EDGE('',*,*,#5970,.T.);
#2574=ORIENTED_EDGE('',*,*,#5954,.F.);
#2575=ORIENTED_EDGE('',*,*,#5951,.F.);
#2576=ORIENTED_EDGE('',*,*,#5971,.T.);
#2577=ORIENTED_EDGE('',*,*,#5972,.T.);
#2578=ORIENTED_EDGE('',*,*,#5957,.F.);
#2579=ORIENTED_EDGE('',*,*,#5973,.T.);
#2580=ORIENTED_EDGE('',*,*,#5974,.T.);
#2581=ORIENTED_EDGE('',*,*,#5975,.T.);
#2582=ORIENTED_EDGE('',*,*,#5960,.F.);
#2583=ORIENTED_EDGE('',*,*,#5976,.T.);
#2584=ORIENTED_EDGE('',*,*,#5977,.T.);
#2585=ORIENTED_EDGE('',*,*,#5978,.T.);
#2586=ORIENTED_EDGE('',*,*,#5966,.F.);
#2587=ORIENTED_EDGE('',*,*,#5963,.F.);
#2588=ORIENTED_EDGE('',*,*,#5979,.T.);
#2589=ORIENTED_EDGE('',*,*,#5980,.F.);
#2590=ORIENTED_EDGE('',*,*,#5970,.F.);
#2591=ORIENTED_EDGE('',*,*,#5981,.F.);
#2592=ORIENTED_EDGE('',*,*,#5982,.T.);
#2593=ORIENTED_EDGE('',*,*,#5983,.F.);
#2594=ORIENTED_EDGE('',*,*,#5973,.F.);
#2595=ORIENTED_EDGE('',*,*,#5984,.F.);
#2596=ORIENTED_EDGE('',*,*,#5985,.T.);
#2597=ORIENTED_EDGE('',*,*,#5986,.F.);
#2598=ORIENTED_EDGE('',*,*,#5971,.F.);
#2599=ORIENTED_EDGE('',*,*,#5987,.F.);
#2600=ORIENTED_EDGE('',*,*,#5988,.T.);
#2601=ORIENTED_EDGE('',*,*,#5989,.F.);
#2602=ORIENTED_EDGE('',*,*,#5974,.F.);
#2603=ORIENTED_EDGE('',*,*,#5990,.F.);
#2604=ORIENTED_EDGE('',*,*,#5991,.T.);
#2605=ORIENTED_EDGE('',*,*,#5992,.F.);
#2606=ORIENTED_EDGE('',*,*,#5975,.F.);
#2607=ORIENTED_EDGE('',*,*,#5993,.F.);
#2608=ORIENTED_EDGE('',*,*,#5994,.T.);
#2609=ORIENTED_EDGE('',*,*,#5995,.F.);
#2610=ORIENTED_EDGE('',*,*,#5977,.F.);
#2611=ORIENTED_EDGE('',*,*,#5996,.F.);
#2612=ORIENTED_EDGE('',*,*,#5997,.T.);
#2613=ORIENTED_EDGE('',*,*,#5998,.T.);
#2614=ORIENTED_EDGE('',*,*,#5982,.F.);
#2615=ORIENTED_EDGE('',*,*,#5979,.F.);
#2616=ORIENTED_EDGE('',*,*,#5985,.F.);
#2617=ORIENTED_EDGE('',*,*,#5999,.T.);
#2618=ORIENTED_EDGE('',*,*,#5988,.F.);
#2619=ORIENTED_EDGE('',*,*,#6000,.T.);
#2620=ORIENTED_EDGE('',*,*,#6001,.T.);
#2621=ORIENTED_EDGE('',*,*,#6002,.T.);
#2622=ORIENTED_EDGE('',*,*,#5994,.F.);
#2623=ORIENTED_EDGE('',*,*,#5991,.F.);
#2624=ORIENTED_EDGE('',*,*,#6003,.T.);
#2625=ORIENTED_EDGE('',*,*,#6004,.F.);
#2626=ORIENTED_EDGE('',*,*,#5998,.F.);
#2627=ORIENTED_EDGE('',*,*,#6005,.F.);
#2628=ORIENTED_EDGE('',*,*,#6006,.T.);
#2629=ORIENTED_EDGE('',*,*,#6007,.F.);
#2630=ORIENTED_EDGE('',*,*,#5999,.F.);
#2631=ORIENTED_EDGE('',*,*,#6008,.F.);
#2632=ORIENTED_EDGE('',*,*,#6009,.T.);
#2633=ORIENTED_EDGE('',*,*,#6010,.F.);
#2634=ORIENTED_EDGE('',*,*,#6001,.F.);
#2635=ORIENTED_EDGE('',*,*,#6011,.F.);
#2636=ORIENTED_EDGE('',*,*,#6003,.F.);
#2637=ORIENTED_EDGE('',*,*,#6012,.T.);
#2638=ORIENTED_EDGE('',*,*,#6009,.F.);
#2639=ORIENTED_EDGE('',*,*,#6006,.F.);
#2640=ORIENTED_EDGE('',*,*,#6013,.T.);
#2641=ORIENTED_EDGE('',*,*,#6014,.F.);
#2642=ORIENTED_EDGE('',*,*,#6015,.T.);
#2643=ORIENTED_EDGE('',*,*,#6016,.F.);
#2644=ORIENTED_EDGE('',*,*,#6017,.T.);
#2645=ORIENTED_EDGE('',*,*,#6018,.F.);
#2646=ORIENTED_EDGE('',*,*,#6019,.T.);
#2647=ORIENTED_EDGE('',*,*,#6020,.T.);
#2648=ORIENTED_EDGE('',*,*,#6021,.T.);
#2649=ORIENTED_EDGE('',*,*,#6022,.T.);
#2650=ORIENTED_EDGE('',*,*,#6023,.T.);
#2651=ORIENTED_EDGE('',*,*,#6024,.T.);
#2652=ORIENTED_EDGE('',*,*,#6025,.F.);
#2653=ORIENTED_EDGE('',*,*,#6026,.T.);
#2654=ORIENTED_EDGE('',*,*,#6027,.T.);
#2655=ORIENTED_EDGE('',*,*,#6028,.T.);
#2656=ORIENTED_EDGE('',*,*,#6029,.F.);
#2657=ORIENTED_EDGE('',*,*,#6030,.F.);
#2658=ORIENTED_EDGE('',*,*,#6031,.F.);
#2659=ORIENTED_EDGE('',*,*,#6032,.F.);
#2660=ORIENTED_EDGE('',*,*,#6033,.T.);
#2661=ORIENTED_EDGE('',*,*,#6025,.T.);
#2662=ORIENTED_EDGE('',*,*,#6034,.T.);
#2663=ORIENTED_EDGE('',*,*,#6027,.F.);
#2664=ORIENTED_EDGE('',*,*,#6034,.F.);
#2665=ORIENTED_EDGE('',*,*,#6024,.F.);
#2666=ORIENTED_EDGE('',*,*,#6035,.F.);
#2667=ORIENTED_EDGE('',*,*,#6028,.F.);
#2668=ORIENTED_EDGE('',*,*,#6033,.F.);
#2669=ORIENTED_EDGE('',*,*,#6026,.F.);
#2670=ORIENTED_EDGE('',*,*,#6036,.F.);
#2671=ORIENTED_EDGE('',*,*,#6019,.F.);
#2672=ORIENTED_EDGE('',*,*,#6037,.T.);
#2673=ORIENTED_EDGE('',*,*,#6038,.T.);
#2674=ORIENTED_EDGE('',*,*,#6039,.F.);
#2675=ORIENTED_EDGE('',*,*,#6040,.F.);
#2676=ORIENTED_EDGE('',*,*,#6041,.F.);
#2677=ORIENTED_EDGE('',*,*,#5883,.F.);
#2678=ORIENTED_EDGE('',*,*,#5899,.T.);
#2679=ORIENTED_EDGE('',*,*,#5916,.F.);
#2680=ORIENTED_EDGE('',*,*,#5930,.T.);
#2681=ORIENTED_EDGE('',*,*,#5944,.F.);
#2682=ORIENTED_EDGE('',*,*,#5958,.T.);
#2683=ORIENTED_EDGE('',*,*,#5972,.F.);
#2684=ORIENTED_EDGE('',*,*,#5986,.T.);
#2685=ORIENTED_EDGE('',*,*,#6000,.F.);
#2686=ORIENTED_EDGE('',*,*,#5990,.T.);
#2687=ORIENTED_EDGE('',*,*,#5976,.F.);
#2688=ORIENTED_EDGE('',*,*,#5962,.T.);
#2689=ORIENTED_EDGE('',*,*,#5948,.F.);
#2690=ORIENTED_EDGE('',*,*,#5934,.T.);
#2691=ORIENTED_EDGE('',*,*,#5920,.F.);
#2692=ORIENTED_EDGE('',*,*,#5903,.T.);
#2693=ORIENTED_EDGE('',*,*,#5888,.F.);
#2694=ORIENTED_EDGE('',*,*,#5875,.T.);
#2695=ORIENTED_EDGE('',*,*,#5869,.F.);
#2696=ORIENTED_EDGE('',*,*,#5863,.T.);
#2697=ORIENTED_EDGE('',*,*,#5858,.T.);
#2698=ORIENTED_EDGE('',*,*,#5865,.F.);
#2699=ORIENTED_EDGE('',*,*,#6042,.T.);
#2700=ORIENTED_EDGE('',*,*,#6043,.T.);
#2701=ORIENTED_EDGE('',*,*,#5931,.T.);
#2702=ORIENTED_EDGE('',*,*,#5927,.T.);
#2703=ORIENTED_EDGE('',*,*,#5952,.T.);
#2704=ORIENTED_EDGE('',*,*,#5956,.T.);
#2705=ORIENTED_EDGE('',*,*,#5900,.T.);
#2706=ORIENTED_EDGE('',*,*,#5896,.T.);
#2707=ORIENTED_EDGE('',*,*,#5924,.T.);
#2708=ORIENTED_EDGE('',*,*,#5928,.T.);
#2709=ORIENTED_EDGE('',*,*,#5897,.T.);
#2710=ORIENTED_EDGE('',*,*,#6044,.T.);
#2711=ORIENTED_EDGE('',*,*,#5871,.T.);
#2712=ORIENTED_EDGE('',*,*,#6045,.T.);
#2713=ORIENTED_EDGE('',*,*,#5872,.T.);
#2714=ORIENTED_EDGE('',*,*,#5860,.T.);
#2715=ORIENTED_EDGE('',*,*,#6046,.T.);
#2716=ORIENTED_EDGE('',*,*,#5894,.T.);
#2717=ORIENTED_EDGE('',*,*,#6046,.F.);
#2718=ORIENTED_EDGE('',*,*,#5862,.T.);
#2719=ORIENTED_EDGE('',*,*,#5877,.T.);
#2720=ORIENTED_EDGE('',*,*,#5911,.T.);
#2721=ORIENTED_EDGE('',*,*,#5874,.T.);
#2722=ORIENTED_EDGE('',*,*,#5905,.T.);
#2723=ORIENTED_EDGE('',*,*,#5909,.T.);
#2724=ORIENTED_EDGE('',*,*,#5878,.T.);
#2725=ORIENTED_EDGE('',*,*,#5933,.T.);
#2726=ORIENTED_EDGE('',*,*,#5964,.T.);
#2727=ORIENTED_EDGE('',*,*,#5968,.T.);
#2728=ORIENTED_EDGE('',*,*,#5937,.T.);
#2729=ORIENTED_EDGE('',*,*,#5961,.T.);
#2730=ORIENTED_EDGE('',*,*,#5992,.T.);
#2731=ORIENTED_EDGE('',*,*,#5996,.T.);
#2732=ORIENTED_EDGE('',*,*,#5965,.T.);
#2733=ORIENTED_EDGE('',*,*,#5989,.T.);
#2734=ORIENTED_EDGE('',*,*,#6007,.T.);
#2735=ORIENTED_EDGE('',*,*,#6011,.T.);
#2736=ORIENTED_EDGE('',*,*,#5993,.T.);
#2737=ORIENTED_EDGE('',*,*,#5987,.T.);
#2738=ORIENTED_EDGE('',*,*,#5983,.T.);
#2739=ORIENTED_EDGE('',*,*,#6004,.T.);
#2740=ORIENTED_EDGE('',*,*,#6008,.T.);
#2741=ORIENTED_EDGE('',*,*,#5959,.T.);
#2742=ORIENTED_EDGE('',*,*,#5955,.T.);
#2743=ORIENTED_EDGE('',*,*,#5980,.T.);
#2744=ORIENTED_EDGE('',*,*,#5984,.T.);
#2745=ORIENTED_EDGE('',*,*,#6002,.F.);
#2746=ORIENTED_EDGE('',*,*,#6010,.T.);
#2747=ORIENTED_EDGE('',*,*,#6012,.F.);
#2748=ORIENTED_EDGE('',*,*,#6005,.T.);
#2749=ORIENTED_EDGE('',*,*,#5997,.F.);
#2750=ORIENTED_EDGE('',*,*,#5981,.T.);
#2751=ORIENTED_EDGE('',*,*,#5969,.F.);
#2752=ORIENTED_EDGE('',*,*,#5953,.T.);
#2753=ORIENTED_EDGE('',*,*,#5941,.F.);
#2754=ORIENTED_EDGE('',*,*,#5925,.T.);
#2755=ORIENTED_EDGE('',*,*,#5912,.F.);
#2756=ORIENTED_EDGE('',*,*,#6047,.T.);
#2757=ORIENTED_EDGE('',*,*,#5879,.F.);
#2758=ORIENTED_EDGE('',*,*,#5893,.T.);
#2759=ORIENTED_EDGE('',*,*,#5910,.T.);
#2760=ORIENTED_EDGE('',*,*,#5889,.F.);
#2761=ORIENTED_EDGE('',*,*,#5908,.T.);
#2762=ORIENTED_EDGE('',*,*,#5922,.F.);
#2763=ORIENTED_EDGE('',*,*,#5939,.T.);
#2764=ORIENTED_EDGE('',*,*,#5950,.F.);
#2765=ORIENTED_EDGE('',*,*,#5967,.T.);
#2766=ORIENTED_EDGE('',*,*,#5978,.F.);
#2767=ORIENTED_EDGE('',*,*,#5995,.T.);
#2768=ORIENTED_EDGE('',*,*,#6048,.T.);
#2769=ORIENTED_EDGE('',*,*,#6049,.T.);
#2770=ORIENTED_EDGE('',*,*,#6050,.T.);
#2771=ORIENTED_EDGE('',*,*,#6051,.T.);
#2772=ORIENTED_EDGE('',*,*,#6023,.F.);
#2773=ORIENTED_EDGE('',*,*,#6022,.F.);
#2774=ORIENTED_EDGE('',*,*,#6021,.F.);
#2775=ORIENTED_EDGE('',*,*,#6020,.F.);
#2776=ORIENTED_EDGE('',*,*,#6036,.T.);
#2777=ORIENTED_EDGE('',*,*,#6051,.F.);
#2778=ORIENTED_EDGE('',*,*,#6032,.T.);
#2779=ORIENTED_EDGE('',*,*,#6031,.T.);
#2780=ORIENTED_EDGE('',*,*,#6030,.T.);
#2781=ORIENTED_EDGE('',*,*,#6029,.T.);
#2782=ORIENTED_EDGE('',*,*,#6035,.T.);
#2783=ORIENTED_EDGE('',*,*,#6037,.F.);
#2784=ORIENTED_EDGE('',*,*,#5902,.T.);
#2785=ORIENTED_EDGE('',*,*,#5936,.T.);
#2786=ORIENTED_EDGE('',*,*,#5940,.T.);
#2787=ORIENTED_EDGE('',*,*,#5906,.T.);
#2788=ORIENTED_EDGE('',*,*,#6018,.T.);
#2789=ORIENTED_EDGE('',*,*,#6050,.F.);
#2790=ORIENTED_EDGE('',*,*,#6039,.T.);
#2791=ORIENTED_EDGE('',*,*,#6017,.F.);
#2792=ORIENTED_EDGE('',*,*,#6016,.T.);
#2793=ORIENTED_EDGE('',*,*,#6049,.F.);
#2794=ORIENTED_EDGE('',*,*,#6040,.T.);
#2795=ORIENTED_EDGE('',*,*,#6015,.F.);
#2796=ORIENTED_EDGE('',*,*,#6014,.T.);
#2797=ORIENTED_EDGE('',*,*,#6048,.F.);
#2798=ORIENTED_EDGE('',*,*,#6041,.T.);
#2799=ORIENTED_EDGE('',*,*,#6013,.F.);
#2800=ORIENTED_EDGE('',*,*,#6047,.F.);
#2801=ORIENTED_EDGE('',*,*,#5914,.T.);
#2802=ORIENTED_EDGE('',*,*,#6045,.F.);
#2803=ORIENTED_EDGE('',*,*,#5880,.F.);
#2804=ORIENTED_EDGE('',*,*,#6044,.F.);
#2805=ORIENTED_EDGE('',*,*,#5884,.T.);
#2806=ORIENTED_EDGE('',*,*,#6042,.F.);
#2807=ORIENTED_EDGE('',*,*,#5864,.F.);
#2808=ORIENTED_EDGE('',*,*,#6043,.F.);
#2809=ORIENTED_EDGE('',*,*,#6052,.F.);
#2810=ORIENTED_EDGE('',*,*,#6052,.T.);
#2811=ORIENTED_EDGE('',*,*,#6038,.F.);
#5857=EDGE_CURVE('',#7643,#7644,#440,.T.);
#5858=EDGE_CURVE('',#7645,#7644,#8821,.T.);
#5859=EDGE_CURVE('',#7645,#7646,#1098,.F.);
#5860=EDGE_CURVE('',#7643,#7646,#8822,.T.);
#5861=EDGE_CURVE('',#7647,#7648,#441,.T.);
#5862=EDGE_CURVE('',#7646,#7648,#442,.T.);
#5863=EDGE_CURVE('',#7647,#7645,#443,.T.);
#5864=EDGE_CURVE('',#7649,#7650,#444,.T.);
#5865=EDGE_CURVE('',#7650,#7644,#445,.T.);
#5866=EDGE_CURVE('',#7643,#7649,#446,.T.);
#5867=EDGE_CURVE('',#7651,#7652,#447,.T.);
#5868=EDGE_CURVE('',#7652,#7648,#448,.T.);
#5869=EDGE_CURVE('',#7647,#7651,#449,.T.);
#5870=EDGE_CURVE('',#7653,#7654,#450,.T.);
#5871=EDGE_CURVE('',#7649,#7654,#8823,.T.);
#5872=EDGE_CURVE('',#7653,#7643,#8824,.T.);
#5873=EDGE_CURVE('',#7655,#7656,#451,.T.);
#5874=EDGE_CURVE('',#7652,#7656,#8825,.T.);
#5875=EDGE_CURVE('',#7655,#7651,#8826,.T.);
#5876=EDGE_CURVE('',#7657,#7658,#452,.T.);
#5877=EDGE_CURVE('',#7648,#7658,#8827,.T.);
#5878=EDGE_CURVE('',#7657,#7652,#8828,.T.);
#5879=EDGE_CURVE('',#7659,#7660,#453,.T.);
#5880=EDGE_CURVE('',#7660,#7654,#454,.T.);
#5881=EDGE_CURVE('',#7653,#7659,#455,.T.);
#5882=EDGE_CURVE('',#7661,#7662,#456,.T.);
#5883=EDGE_CURVE('',#7662,#7663,#457,.T.);
#5884=EDGE_CURVE('',#7664,#7663,#458,.T.);
#5885=EDGE_CURVE('',#7664,#7661,#459,.T.);
#5886=EDGE_CURVE('',#7665,#7666,#460,.T.);
#5887=EDGE_CURVE('',#7666,#7656,#461,.T.);
#5888=EDGE_CURVE('',#7655,#7665,#462,.T.);
#5889=EDGE_CURVE('',#7667,#7668,#463,.T.);
#5890=EDGE_CURVE('',#7668,#7658,#464,.T.);
#5891=EDGE_CURVE('',#7657,#7667,#465,.T.);
#5892=EDGE_CURVE('',#7669,#7670,#1099,.T.);
#5893=EDGE_CURVE('',#7659,#7670,#8829,.T.);
#5894=EDGE_CURVE('',#7669,#7653,#8830,.T.);
#5895=EDGE_CURVE('',#7671,#7672,#466,.T.);
#5896=EDGE_CURVE('',#7661,#7672,#8831,.T.);
#5897=EDGE_CURVE('',#7671,#7664,#8832,.T.);
#5898=EDGE_CURVE('',#7673,#7674,#467,.T.);
#5899=EDGE_CURVE('',#7662,#7674,#8833,.T.);
#5900=EDGE_CURVE('',#7673,#7661,#8834,.T.);
#5901=EDGE_CURVE('',#7675,#7676,#468,.T.);
#5902=EDGE_CURVE('',#7666,#7676,#469,.T.);
#5903=EDGE_CURVE('',#7675,#7665,#470,.T.);
#5904=EDGE_CURVE('',#7677,#7678,#471,.T.);
#5905=EDGE_CURVE('',#7656,#7678,#8835,.T.);
#5906=EDGE_CURVE('',#7677,#7666,#8836,.T.);
#5907=EDGE_CURVE('',#7678,#7679,#472,.T.);
#5908=EDGE_CURVE('',#7667,#7679,#8837,.T.);
#5909=EDGE_CURVE('',#7678,#7657,#8838,.T.);
#5910=EDGE_CURVE('',#7670,#7668,#473,.T.);
#5911=EDGE_CURVE('',#7658,#7669,#474,.T.);
#5912=EDGE_CURVE('',#7680,#7681,#475,.T.);
#5913=EDGE_CURVE('',#7681,#7672,#476,.T.);
#5914=EDGE_CURVE('',#7680,#7671,#477,.T.);
#5915=EDGE_CURVE('',#7682,#7683,#478,.T.);
#5916=EDGE_CURVE('',#7683,#7674,#479,.T.);
#5917=EDGE_CURVE('',#7673,#7682,#480,.T.);
#5918=EDGE_CURVE('',#7684,#7685,#481,.T.);
#5919=EDGE_CURVE('',#7685,#7676,#482,.T.);
#5920=EDGE_CURVE('',#7675,#7684,#483,.T.);
#5921=EDGE_CURVE('',#7677,#7686,#484,.T.);
#5922=EDGE_CURVE('',#7686,#7679,#485,.T.);
#5923=EDGE_CURVE('',#7687,#7688,#486,.T.);
#5924=EDGE_CURVE('',#7672,#7688,#8839,.T.);
#5925=EDGE_CURVE('',#7687,#7681,#8840,.T.);
#5926=EDGE_CURVE('',#7688,#7689,#487,.T.);
#5927=EDGE_CURVE('',#7682,#7689,#8841,.T.);
#5928=EDGE_CURVE('',#7688,#7673,#8842,.T.);
#5929=EDGE_CURVE('',#7690,#7691,#488,.T.);
#5930=EDGE_CURVE('',#7683,#7691,#489,.T.);
#5931=EDGE_CURVE('',#7690,#7682,#490,.T.);
#5932=EDGE_CURVE('',#7692,#7693,#491,.T.);
#5933=EDGE_CURVE('',#7685,#7693,#8843,.T.);
#5934=EDGE_CURVE('',#7692,#7684,#8844,.T.);
#5935=EDGE_CURVE('',#7694,#7695,#492,.T.);
#5936=EDGE_CURVE('',#7676,#7695,#8845,.T.);
#5937=EDGE_CURVE('',#7694,#7685,#8846,.T.);
#5938=EDGE_CURVE('',#7695,#7696,#493,.T.);
#5939=EDGE_CURVE('',#7686,#7696,#494,.T.);
#5940=EDGE_CURVE('',#7695,#7677,#495,.T.);
#5941=EDGE_CURVE('',#7687,#7697,#496,.T.);
#5942=EDGE_CURVE('',#7697,#7689,#497,.T.);
#5943=EDGE_CURVE('',#7698,#7699,#498,.T.);
#5944=EDGE_CURVE('',#7699,#7691,#499,.T.);
#5945=EDGE_CURVE('',#7690,#7698,#500,.T.);
#5946=EDGE_CURVE('',#7700,#7701,#501,.T.);
#5947=EDGE_CURVE('',#7701,#7693,#502,.T.);
#5948=EDGE_CURVE('',#7692,#7700,#503,.T.);
#5949=EDGE_CURVE('',#7694,#7702,#504,.T.);
#5950=EDGE_CURVE('',#7702,#7696,#505,.T.);
#5951=EDGE_CURVE('',#7703,#7704,#506,.T.);
#5952=EDGE_CURVE('',#7689,#7704,#507,.T.);
#5953=EDGE_CURVE('',#7703,#7697,#508,.T.);
#5954=EDGE_CURVE('',#7704,#7705,#509,.T.);
#5955=EDGE_CURVE('',#7698,#7705,#8847,.T.);
#5956=EDGE_CURVE('',#7704,#7690,#8848,.T.);
#5957=EDGE_CURVE('',#7706,#7707,#510,.T.);
#5958=EDGE_CURVE('',#7699,#7707,#8849,.T.);
#5959=EDGE_CURVE('',#7706,#7698,#8850,.T.);
#5960=EDGE_CURVE('',#7708,#7709,#511,.T.);
#5961=EDGE_CURVE('',#7701,#7709,#512,.T.);
#5962=EDGE_CURVE('',#7708,#7700,#513,.T.);
#5963=EDGE_CURVE('',#7710,#7711,#514,.T.);
#5964=EDGE_CURVE('',#7693,#7711,#8851,.T.);
#5965=EDGE_CURVE('',#7710,#7701,#8852,.T.);
#5966=EDGE_CURVE('',#7711,#7712,#515,.T.);
#5967=EDGE_CURVE('',#7702,#7712,#8853,.T.);
#5968=EDGE_CURVE('',#7711,#7694,#8854,.T.);
#5969=EDGE_CURVE('',#7703,#7713,#516,.T.);
#5970=EDGE_CURVE('',#7713,#7705,#517,.T.);
#5971=EDGE_CURVE('',#7714,#7715,#518,.T.);
#5972=EDGE_CURVE('',#7715,#7707,#519,.T.);
#5973=EDGE_CURVE('',#7706,#7714,#520,.T.);
#5974=EDGE_CURVE('',#7716,#7717,#521,.T.);
#5975=EDGE_CURVE('',#7717,#7709,#522,.T.);
#5976=EDGE_CURVE('',#7708,#7716,#523,.T.);
#5977=EDGE_CURVE('',#7710,#7718,#524,.T.);
#5978=EDGE_CURVE('',#7718,#7712,#525,.T.);
#5979=EDGE_CURVE('',#7719,#7720,#526,.T.);
#5980=EDGE_CURVE('',#7705,#7720,#8855,.T.);
#5981=EDGE_CURVE('',#7719,#7713,#8856,.T.);
#5982=EDGE_CURVE('',#7720,#7721,#527,.T.);
#5983=EDGE_CURVE('',#7714,#7721,#8857,.T.);
#5984=EDGE_CURVE('',#7720,#7706,#8858,.T.);
#5985=EDGE_CURVE('',#7722,#7723,#528,.T.);
#5986=EDGE_CURVE('',#7715,#7723,#529,.T.);
#5987=EDGE_CURVE('',#7722,#7714,#530,.T.);
#5988=EDGE_CURVE('',#7724,#7725,#531,.T.);
#5989=EDGE_CURVE('',#7717,#7725,#8859,.T.);
#5990=EDGE_CURVE('',#7724,#7716,#8860,.T.);
#5991=EDGE_CURVE('',#7726,#7727,#532,.T.);
#5992=EDGE_CURVE('',#7709,#7727,#8861,.T.);
#5993=EDGE_CURVE('',#7726,#7717,#8862,.T.);
#5994=EDGE_CURVE('',#7727,#7728,#533,.T.);
#5995=EDGE_CURVE('',#7718,#7728,#534,.T.);
#5996=EDGE_CURVE('',#7727,#7710,#535,.T.);
#5997=EDGE_CURVE('',#7719,#7729,#536,.T.);
#5998=EDGE_CURVE('',#7729,#7721,#537,.T.);
#5999=EDGE_CURVE('',#7722,#7725,#538,.T.);
#6000=EDGE_CURVE('',#7724,#7723,#539,.T.);
#6001=EDGE_CURVE('',#7726,#7730,#540,.T.);
#6002=EDGE_CURVE('',#7730,#7728,#541,.T.);
#6003=EDGE_CURVE('',#7731,#7732,#542,.T.);
#6004=EDGE_CURVE('',#7721,#7732,#543,.T.);
#6005=EDGE_CURVE('',#7731,#7729,#544,.T.);
#6006=EDGE_CURVE('',#7732,#7733,#545,.T.);
#6007=EDGE_CURVE('',#7725,#7733,#8863,.T.);
#6008=EDGE_CURVE('',#7732,#7722,#8864,.T.);
#6009=EDGE_CURVE('',#7733,#7734,#546,.T.);
#6010=EDGE_CURVE('',#7730,#7734,#8865,.T.);
#6011=EDGE_CURVE('',#7733,#7726,#8866,.T.);
#6012=EDGE_CURVE('',#7731,#7734,#547,.T.);
#6013=EDGE_CURVE('',#7735,#7735,#548,.T.);
#6014=EDGE_CURVE('',#7736,#7736,#549,.T.);
#6015=EDGE_CURVE('',#7737,#7737,#550,.T.);
#6016=EDGE_CURVE('',#7738,#7738,#551,.T.);
#6017=EDGE_CURVE('',#7739,#7739,#552,.T.);
#6018=EDGE_CURVE('',#7740,#7740,#553,.T.);
#6019=EDGE_CURVE('',#7741,#7742,#8867,.T.);
#6020=EDGE_CURVE('',#7742,#7743,#1866,.T.);
#6021=EDGE_CURVE('',#7743,#7744,#1867,.T.);
#6022=EDGE_CURVE('',#7744,#7745,#1868,.T.);
#6023=EDGE_CURVE('',#7745,#7746,#1869,.T.);
#6024=EDGE_CURVE('',#7746,#7747,#8868,.T.);
#6025=EDGE_CURVE('',#7741,#7747,#1870,.T.);
#6026=EDGE_CURVE('',#7748,#7749,#8869,.T.);
#6027=EDGE_CURVE('',#7749,#7750,#1871,.T.);
#6028=EDGE_CURVE('',#7750,#7751,#8870,.T.);
#6029=EDGE_CURVE('',#7752,#7751,#1872,.T.);
#6030=EDGE_CURVE('',#7753,#7752,#1873,.T.);
#6031=EDGE_CURVE('',#7754,#7753,#1874,.T.);
#6032=EDGE_CURVE('',#7748,#7754,#1875,.T.);
#6033=EDGE_CURVE('',#7749,#7741,#8871,.T.);
#6034=EDGE_CURVE('',#7747,#7750,#8872,.T.);
#6035=EDGE_CURVE('',#7751,#7746,#8873,.T.);
#6036=EDGE_CURVE('',#7742,#7748,#8874,.T.);
#6037=EDGE_CURVE('',#7755,#7755,#554,.T.);
#6038=EDGE_CURVE('',#7756,#7756,#555,.T.);
#6039=EDGE_CURVE('',#7757,#7757,#556,.T.);
#6040=EDGE_CURVE('',#7758,#7758,#557,.T.);
#6041=EDGE_CURVE('',#7759,#7759,#558,.T.);
#6042=EDGE_CURVE('',#7650,#7663,#559,.T.);
#6043=EDGE_CURVE('',#7760,#7760,#560,.T.);
#6044=EDGE_CURVE('',#7664,#7649,#561,.T.);
#6045=EDGE_CURVE('',#7654,#7671,#562,.T.);
#6046=EDGE_CURVE('',#7646,#7669,#8875,.T.);
#6047=EDGE_CURVE('',#7680,#7660,#563,.T.);
#6048=EDGE_CURVE('',#7761,#7761,#564,.T.);
#6049=EDGE_CURVE('',#7762,#7762,#565,.T.);
#6050=EDGE_CURVE('',#7763,#7763,#566,.T.);
#6051=EDGE_CURVE('',#7748,#7748,#567,.T.);
#6052=EDGE_CURVE('',#7764,#7764,#568,.T.);
#7643=VERTEX_POINT('',#30743);
#7644=VERTEX_POINT('',#30744);
#7645=VERTEX_POINT('',#30746);
#7646=VERTEX_POINT('',#30752);
#7647=VERTEX_POINT('',#30756);
#7648=VERTEX_POINT('',#30757);
#7649=VERTEX_POINT('',#30762);
#7650=VERTEX_POINT('',#30763);
#7651=VERTEX_POINT('',#30768);
#7652=VERTEX_POINT('',#30769);
#7653=VERTEX_POINT('',#30774);
#7654=VERTEX_POINT('',#30775);
#7655=VERTEX_POINT('',#30780);
#7656=VERTEX_POINT('',#30781);
#7657=VERTEX_POINT('',#30786);
#7658=VERTEX_POINT('',#30787);
#7659=VERTEX_POINT('',#30792);
#7660=VERTEX_POINT('',#30793);
#7661=VERTEX_POINT('',#30798);
#7662=VERTEX_POINT('',#30799);
#7663=VERTEX_POINT('',#30801);
#7664=VERTEX_POINT('',#30803);
#7665=VERTEX_POINT('',#30807);
#7666=VERTEX_POINT('',#30808);
#7667=VERTEX_POINT('',#30813);
#7668=VERTEX_POINT('',#30814);
#7669=VERTEX_POINT('',#30823);
#7670=VERTEX_POINT('',#30824);
#7671=VERTEX_POINT('',#30829);
#7672=VERTEX_POINT('',#30830);
#7673=VERTEX_POINT('',#30835);
#7674=VERTEX_POINT('',#30836);
#7675=VERTEX_POINT('',#30841);
#7676=VERTEX_POINT('',#30842);
#7677=VERTEX_POINT('',#30847);
#7678=VERTEX_POINT('',#30848);
#7679=VERTEX_POINT('',#30853);
#7680=VERTEX_POINT('',#30861);
#7681=VERTEX_POINT('',#30862);
#7682=VERTEX_POINT('',#30867);
#7683=VERTEX_POINT('',#30868);
#7684=VERTEX_POINT('',#30873);
#7685=VERTEX_POINT('',#30874);
#7686=VERTEX_POINT('',#30879);
#7687=VERTEX_POINT('',#30883);
#7688=VERTEX_POINT('',#30884);
#7689=VERTEX_POINT('',#30889);
#7690=VERTEX_POINT('',#30894);
#7691=VERTEX_POINT('',#30895);
#7692=VERTEX_POINT('',#30900);
#7693=VERTEX_POINT('',#30901);
#7694=VERTEX_POINT('',#30906);
#7695=VERTEX_POINT('',#30907);
#7696=VERTEX_POINT('',#30912);
#7697=VERTEX_POINT('',#30917);
#7698=VERTEX_POINT('',#30921);
#7699=VERTEX_POINT('',#30922);
#7700=VERTEX_POINT('',#30927);
#7701=VERTEX_POINT('',#30928);
#7702=VERTEX_POINT('',#30933);
#7703=VERTEX_POINT('',#30937);
#7704=VERTEX_POINT('',#30938);
#7705=VERTEX_POINT('',#30943);
#7706=VERTEX_POINT('',#30948);
#7707=VERTEX_POINT('',#30949);
#7708=VERTEX_POINT('',#30954);
#7709=VERTEX_POINT('',#30955);
#7710=VERTEX_POINT('',#30960);
#7711=VERTEX_POINT('',#30961);
#7712=VERTEX_POINT('',#30966);
#7713=VERTEX_POINT('',#30971);
#7714=VERTEX_POINT('',#30975);
#7715=VERTEX_POINT('',#30976);
#7716=VERTEX_POINT('',#30981);
#7717=VERTEX_POINT('',#30982);
#7718=VERTEX_POINT('',#30987);
#7719=VERTEX_POINT('',#30991);
#7720=VERTEX_POINT('',#30992);
#7721=VERTEX_POINT('',#30997);
#7722=VERTEX_POINT('',#31002);
#7723=VERTEX_POINT('',#31003);
#7724=VERTEX_POINT('',#31008);
#7725=VERTEX_POINT('',#31009);
#7726=VERTEX_POINT('',#31014);
#7727=VERTEX_POINT('',#31015);
#7728=VERTEX_POINT('',#31020);
#7729=VERTEX_POINT('',#31025);
#7730=VERTEX_POINT('',#31032);
#7731=VERTEX_POINT('',#31036);
#7732=VERTEX_POINT('',#31037);
#7733=VERTEX_POINT('',#31042);
#7734=VERTEX_POINT('',#31047);
#7735=VERTEX_POINT('',#31054);
#7736=VERTEX_POINT('',#31056);
#7737=VERTEX_POINT('',#31059);
#7738=VERTEX_POINT('',#31061);
#7739=VERTEX_POINT('',#31064);
#7740=VERTEX_POINT('',#31066);
#7741=VERTEX_POINT('',#31138);
#7742=VERTEX_POINT('',#31139);
#7743=VERTEX_POINT('',#31151);
#7744=VERTEX_POINT('',#31163);
#7745=VERTEX_POINT('',#31175);
#7746=VERTEX_POINT('',#31181);
#7747=VERTEX_POINT('',#31183);
#7748=VERTEX_POINT('',#31452);
#7749=VERTEX_POINT('',#31453);
#7750=VERTEX_POINT('',#31489);
#7751=VERTEX_POINT('',#31491);
#7752=VERTEX_POINT('',#31497);
#7753=VERTEX_POINT('',#31509);
#7754=VERTEX_POINT('',#31521);
#7755=VERTEX_POINT('',#31542);
#7756=VERTEX_POINT('',#31544);
#7757=VERTEX_POINT('',#31547);
#7758=VERTEX_POINT('',#31549);
#7759=VERTEX_POINT('',#31551);
#7760=VERTEX_POINT('',#31554);
#7761=VERTEX_POINT('',#31572);
#7762=VERTEX_POINT('',#31574);
#7763=VERTEX_POINT('',#31576);
#7764=VERTEX_POINT('',#31590);
#8821=LINE('',#30745,#9649);
#8822=LINE('',#30753,#9650);
#8823=LINE('',#30776,#9651);
#8824=LINE('',#30777,#9652);
#8825=LINE('',#30782,#9653);
#8826=LINE('',#30783,#9654);
#8827=LINE('',#30788,#9655);
#8828=LINE('',#30789,#9656);
#8829=LINE('',#30825,#9657);
#8830=LINE('',#30826,#9658);
#8831=LINE('',#30831,#9659);
#8832=LINE('',#30832,#9660);
#8833=LINE('',#30837,#9661);
#8834=LINE('',#30838,#9662);
#8835=LINE('',#30849,#9663);
#8836=LINE('',#30850,#9664);
#8837=LINE('',#30854,#9665);
#8838=LINE('',#30855,#9666);
#8839=LINE('',#30885,#9667);
#8840=LINE('',#30886,#9668);
#8841=LINE('',#30890,#9669);
#8842=LINE('',#30891,#9670);
#8843=LINE('',#30902,#9671);
#8844=LINE('',#30903,#9672);
#8845=LINE('',#30908,#9673);
#8846=LINE('',#30909,#9674);
#8847=LINE('',#30944,#9675);
#8848=LINE('',#30945,#9676);
#8849=LINE('',#30950,#9677);
#8850=LINE('',#30951,#9678);
#8851=LINE('',#30962,#9679);
#8852=LINE('',#30963,#9680);
#8853=LINE('',#30967,#9681);
#8854=LINE('',#30968,#9682);
#8855=LINE('',#30993,#9683);
#8856=LINE('',#30994,#9684);
#8857=LINE('',#30998,#9685);
#8858=LINE('',#30999,#9686);
#8859=LINE('',#31010,#9687);
#8860=LINE('',#31011,#9688);
#8861=LINE('',#31016,#9689);
#8862=LINE('',#31017,#9690);
#8863=LINE('',#31043,#9691);
#8864=LINE('',#31044,#9692);
#8865=LINE('',#31048,#9693);
#8866=LINE('',#31049,#9694);
#8867=LINE('',#31137,#9695);
#8868=LINE('',#31182,#9696);
#8869=LINE('',#31451,#9697);
#8870=LINE('',#31490,#9698);
#8871=LINE('',#31534,#9699);
#8872=LINE('',#31535,#9700);
#8873=LINE('',#31537,#9701);
#8874=LINE('',#31539,#9702);
#8875=LINE('',#31561,#9703);
#9649=VECTOR('',#15761,1.);
#9650=VECTOR('',#15762,1.);
#9651=VECTOR('',#15791,1.);
#9652=VECTOR('',#15792,1.);
#9653=VECTOR('',#15797,1.);
#9654=VECTOR('',#15798,1.);
#9655=VECTOR('',#15803,1.);
#9656=VECTOR('',#15804,1.);
#9657=VECTOR('',#15841,1.);
#9658=VECTOR('',#15842,1.);
#9659=VECTOR('',#15847,1.);
#9660=VECTOR('',#15848,1.);
#9661=VECTOR('',#15853,1.);
#9662=VECTOR('',#15854,1.);
#9663=VECTOR('',#15867,1.);
#9664=VECTOR('',#15868,1.);
#9665=VECTOR('',#15873,1.);
#9666=VECTOR('',#15874,1.);
#9667=VECTOR('',#15915,1.);
#9668=VECTOR('',#15916,1.);
#9669=VECTOR('',#15921,1.);
#9670=VECTOR('',#15922,1.);
#9671=VECTOR('',#15935,1.);
#9672=VECTOR('',#15936,1.);
#9673=VECTOR('',#15941,1.);
#9674=VECTOR('',#15942,1.);
#9675=VECTOR('',#15991,1.);
#9676=VECTOR('',#15992,1.);
#9677=VECTOR('',#15997,1.);
#9678=VECTOR('',#15998,1.);
#9679=VECTOR('',#16011,1.);
#9680=VECTOR('',#16012,1.);
#9681=VECTOR('',#16017,1.);
#9682=VECTOR('',#16018,1.);
#9683=VECTOR('',#16051,1.);
#9684=VECTOR('',#16052,1.);
#9685=VECTOR('',#16057,1.);
#9686=VECTOR('',#16058,1.);
#9687=VECTOR('',#16071,1.);
#9688=VECTOR('',#16072,1.);
#9689=VECTOR('',#16077,1.);
#9690=VECTOR('',#16078,1.);
#9691=VECTOR('',#16117,1.);
#9692=VECTOR('',#16118,1.);
#9693=VECTOR('',#16123,1.);
#9694=VECTOR('',#16124,1.);
#9695=VECTOR('',#16147,1.);
#9696=VECTOR('',#16148,1.);
#9697=VECTOR('',#16149,1.);
#9698=VECTOR('',#16150,1.);
#9699=VECTOR('',#16153,1.);
#9700=VECTOR('',#16154,1.);
#9701=VECTOR('',#16157,1.);
#9702=VECTOR('',#16160,1.);
#9703=VECTOR('',#16191,1.);
#10645=EDGE_LOOP('',(#2420,#2421,#2422,#2423));
#10646=EDGE_LOOP('',(#2424,#2425,#2426,#2427));
#10647=EDGE_LOOP('',(#2428,#2429,#2430,#2431));
#10648=EDGE_LOOP('',(#2432,#2433,#2434,#2435));
#10649=EDGE_LOOP('',(#2436,#2437,#2438,#2439));
#10650=EDGE_LOOP('',(#2440,#2441,#2442,#2443));
#10651=EDGE_LOOP('',(#2444,#2445,#2446,#2447));
#10652=EDGE_LOOP('',(#2448,#2449,#2450,#2451));
#10653=EDGE_LOOP('',(#2452,#2453,#2454,#2455));
#10654=EDGE_LOOP('',(#2456,#2457,#2458,#2459));
#10655=EDGE_LOOP('',(#2460,#2461,#2462,#2463));
#10656=EDGE_LOOP('',(#2464,#2465,#2466,#2467));
#10657=EDGE_LOOP('',(#2468,#2469,#2470,#2471));
#10658=EDGE_LOOP('',(#2472,#2473,#2474,#2475));
#10659=EDGE_LOOP('',(#2476,#2477,#2478,#2479));
#10660=EDGE_LOOP('',(#2480,#2481,#2482,#2483));
#10661=EDGE_LOOP('',(#2484,#2485,#2486,#2487));
#10662=EDGE_LOOP('',(#2488,#2489,#2490,#2491));
#10663=EDGE_LOOP('',(#2492,#2493,#2494,#2495));
#10664=EDGE_LOOP('',(#2496,#2497,#2498,#2499));
#10665=EDGE_LOOP('',(#2500,#2501,#2502,#2503));
#10666=EDGE_LOOP('',(#2504,#2505,#2506,#2507));
#10667=EDGE_LOOP('',(#2508,#2509,#2510,#2511));
#10668=EDGE_LOOP('',(#2512,#2513,#2514,#2515));
#10669=EDGE_LOOP('',(#2516,#2517,#2518,#2519));
#10670=EDGE_LOOP('',(#2520,#2521,#2522,#2523));
#10671=EDGE_LOOP('',(#2524,#2525,#2526,#2527));
#10672=EDGE_LOOP('',(#2528,#2529,#2530,#2531));
#10673=EDGE_LOOP('',(#2532,#2533,#2534,#2535));
#10674=EDGE_LOOP('',(#2536,#2537,#2538,#2539));
#10675=EDGE_LOOP('',(#2540,#2541,#2542,#2543));
#10676=EDGE_LOOP('',(#2544,#2545,#2546,#2547));
#10677=EDGE_LOOP('',(#2548,#2549,#2550,#2551));
#10678=EDGE_LOOP('',(#2552,#2553,#2554,#2555));
#10679=EDGE_LOOP('',(#2556,#2557,#2558,#2559));
#10680=EDGE_LOOP('',(#2560,#2561,#2562,#2563));
#10681=EDGE_LOOP('',(#2564,#2565,#2566,#2567));
#10682=EDGE_LOOP('',(#2568,#2569,#2570,#2571));
#10683=EDGE_LOOP('',(#2572,#2573,#2574,#2575));
#10684=EDGE_LOOP('',(#2576,#2577,#2578,#2579));
#10685=EDGE_LOOP('',(#2580,#2581,#2582,#2583));
#10686=EDGE_LOOP('',(#2584,#2585,#2586,#2587));
#10687=EDGE_LOOP('',(#2588,#2589,#2590,#2591));
#10688=EDGE_LOOP('',(#2592,#2593,#2594,#2595));
#10689=EDGE_LOOP('',(#2596,#2597,#2598,#2599));
#10690=EDGE_LOOP('',(#2600,#2601,#2602,#2603));
#10691=EDGE_LOOP('',(#2604,#2605,#2606,#2607));
#10692=EDGE_LOOP('',(#2608,#2609,#2610,#2611));
#10693=EDGE_LOOP('',(#2612,#2613,#2614,#2615));
#10694=EDGE_LOOP('',(#2616,#2617,#2618,#2619));
#10695=EDGE_LOOP('',(#2620,#2621,#2622,#2623));
#10696=EDGE_LOOP('',(#2624,#2625,#2626,#2627));
#10697=EDGE_LOOP('',(#2628,#2629,#2630,#2631));
#10698=EDGE_LOOP('',(#2632,#2633,#2634,#2635));
#10699=EDGE_LOOP('',(#2636,#2637,#2638,#2639));
#10700=EDGE_LOOP('',(#2640));
#10701=EDGE_LOOP('',(#2641));
#10702=EDGE_LOOP('',(#2642));
#10703=EDGE_LOOP('',(#2643));
#10704=EDGE_LOOP('',(#2644));
#10705=EDGE_LOOP('',(#2645));
#10706=EDGE_LOOP('',(#2646,#2647,#2648,#2649,#2650,#2651,#2652));
#10707=EDGE_LOOP('',(#2653,#2654,#2655,#2656,#2657,#2658,#2659));
#10708=EDGE_LOOP('',(#2660,#2661,#2662,#2663));
#10709=EDGE_LOOP('',(#2664,#2665,#2666,#2667));
#10710=EDGE_LOOP('',(#2668,#2669,#2670,#2671));
#10711=EDGE_LOOP('',(#2672));
#10712=EDGE_LOOP('',(#2673));
#10713=EDGE_LOOP('',(#2674));
#10714=EDGE_LOOP('',(#2675));
#10715=EDGE_LOOP('',(#2676));
#10716=EDGE_LOOP('',(#2677,#2678,#2679,#2680,#2681,#2682,#2683,#2684,#2685,
#2686,#2687,#2688,#2689,#2690,#2691,#2692,#2693,#2694,#2695,#2696,#2697,
#2698,#2699));
#10717=EDGE_LOOP('',(#2700));
#10718=EDGE_LOOP('',(#2701,#2702,#2703,#2704));
#10719=EDGE_LOOP('',(#2705,#2706,#2707,#2708));
#10720=EDGE_LOOP('',(#2709,#2710,#2711,#2712));
#10721=EDGE_LOOP('',(#2713,#2714,#2715,#2716));
#10722=EDGE_LOOP('',(#2717,#2718,#2719,#2720));
#10723=EDGE_LOOP('',(#2721,#2722,#2723,#2724));
#10724=EDGE_LOOP('',(#2725,#2726,#2727,#2728));
#10725=EDGE_LOOP('',(#2729,#2730,#2731,#2732));
#10726=EDGE_LOOP('',(#2733,#2734,#2735,#2736));
#10727=EDGE_LOOP('',(#2737,#2738,#2739,#2740));
#10728=EDGE_LOOP('',(#2741,#2742,#2743,#2744));
#10729=EDGE_LOOP('',(#2745,#2746,#2747,#2748,#2749,#2750,#2751,#2752,#2753,
#2754,#2755,#2756,#2757,#2758,#2759,#2760,#2761,#2762,#2763,#2764,#2765,
#2766,#2767));
#10730=EDGE_LOOP('',(#2768));
#10731=EDGE_LOOP('',(#2769));
#10732=EDGE_LOOP('',(#2770));
#10733=EDGE_LOOP('',(#2771));
#10734=EDGE_LOOP('',(#2772,#2773,#2774,#2775,#2776,#2777,#2778,#2779,#2780,
#2781,#2782));
#10735=EDGE_LOOP('',(#2783));
#10736=EDGE_LOOP('',(#2784,#2785,#2786,#2787));
#10737=EDGE_LOOP('',(#2788));
#10738=EDGE_LOOP('',(#2789));
#10739=EDGE_LOOP('',(#2790));
#10740=EDGE_LOOP('',(#2791));
#10741=EDGE_LOOP('',(#2792));
#10742=EDGE_LOOP('',(#2793));
#10743=EDGE_LOOP('',(#2794));
#10744=EDGE_LOOP('',(#2795));
#10745=EDGE_LOOP('',(#2796));
#10746=EDGE_LOOP('',(#2797));
#10747=EDGE_LOOP('',(#2798));
#10748=EDGE_LOOP('',(#2799));
#10749=EDGE_LOOP('',(#2800,#2801,#2802,#2803));
#10750=EDGE_LOOP('',(#2804,#2805,#2806,#2807));
#10751=EDGE_LOOP('',(#2808));
#10752=EDGE_LOOP('',(#2809));
#10753=EDGE_LOOP('',(#2810));
#10754=EDGE_LOOP('',(#2811));
#11760=FACE_BOUND('',#10645,.T.);
#11761=FACE_BOUND('',#10646,.T.);
#11762=FACE_BOUND('',#10647,.T.);
#11763=FACE_BOUND('',#10648,.T.);
#11764=FACE_BOUND('',#10649,.T.);
#11765=FACE_BOUND('',#10650,.T.);
#11766=FACE_BOUND('',#10651,.T.);
#11767=FACE_BOUND('',#10652,.T.);
#11768=FACE_BOUND('',#10653,.T.);
#11769=FACE_BOUND('',#10654,.T.);
#11770=FACE_BOUND('',#10655,.T.);
#11771=FACE_BOUND('',#10656,.T.);
#11772=FACE_BOUND('',#10657,.T.);
#11773=FACE_BOUND('',#10658,.T.);
#11774=FACE_BOUND('',#10659,.T.);
#11775=FACE_BOUND('',#10660,.T.);
#11776=FACE_BOUND('',#10661,.T.);
#11777=FACE_BOUND('',#10662,.T.);
#11778=FACE_BOUND('',#10663,.T.);
#11779=FACE_BOUND('',#10664,.T.);
#11780=FACE_BOUND('',#10665,.T.);
#11781=FACE_BOUND('',#10666,.T.);
#11782=FACE_BOUND('',#10667,.T.);
#11783=FACE_BOUND('',#10668,.T.);
#11784=FACE_BOUND('',#10669,.T.);
#11785=FACE_BOUND('',#10670,.T.);
#11786=FACE_BOUND('',#10671,.T.);
#11787=FACE_BOUND('',#10672,.T.);
#11788=FACE_BOUND('',#10673,.T.);
#11789=FACE_BOUND('',#10674,.T.);
#11790=FACE_BOUND('',#10675,.T.);
#11791=FACE_BOUND('',#10676,.T.);
#11792=FACE_BOUND('',#10677,.T.);
#11793=FACE_BOUND('',#10678,.T.);
#11794=FACE_BOUND('',#10679,.T.);
#11795=FACE_BOUND('',#10680,.T.);
#11796=FACE_BOUND('',#10681,.T.);
#11797=FACE_BOUND('',#10682,.T.);
#11798=FACE_BOUND('',#10683,.T.);
#11799=FACE_BOUND('',#10684,.T.);
#11800=FACE_BOUND('',#10685,.T.);
#11801=FACE_BOUND('',#10686,.T.);
#11802=FACE_BOUND('',#10687,.T.);
#11803=FACE_BOUND('',#10688,.T.);
#11804=FACE_BOUND('',#10689,.T.);
#11805=FACE_BOUND('',#10690,.T.);
#11806=FACE_BOUND('',#10691,.T.);
#11807=FACE_BOUND('',#10692,.T.);
#11808=FACE_BOUND('',#10693,.T.);
#11809=FACE_BOUND('',#10694,.T.);
#11810=FACE_BOUND('',#10695,.T.);
#11811=FACE_BOUND('',#10696,.T.);
#11812=FACE_BOUND('',#10697,.T.);
#11813=FACE_BOUND('',#10698,.T.);
#11814=FACE_BOUND('',#10699,.T.);
#11815=FACE_BOUND('',#10700,.T.);
#11816=FACE_BOUND('',#10701,.T.);
#11817=FACE_BOUND('',#10702,.T.);
#11818=FACE_BOUND('',#10703,.T.);
#11819=FACE_BOUND('',#10704,.T.);
#11820=FACE_BOUND('',#10705,.T.);
#11821=FACE_BOUND('',#10706,.T.);
#11822=FACE_BOUND('',#10707,.T.);
#11823=FACE_BOUND('',#10708,.T.);
#11824=FACE_BOUND('',#10709,.T.);
#11825=FACE_BOUND('',#10710,.T.);
#11826=FACE_BOUND('',#10711,.T.);
#11827=FACE_BOUND('',#10712,.T.);
#11828=FACE_BOUND('',#10713,.T.);
#11829=FACE_BOUND('',#10714,.T.);
#11830=FACE_BOUND('',#10715,.T.);
#11831=FACE_BOUND('',#10716,.T.);
#11832=FACE_BOUND('',#10717,.T.);
#11833=FACE_BOUND('',#10718,.T.);
#11834=FACE_BOUND('',#10719,.T.);
#11835=FACE_BOUND('',#10720,.T.);
#11836=FACE_BOUND('',#10721,.T.);
#11837=FACE_BOUND('',#10722,.T.);
#11838=FACE_BOUND('',#10723,.T.);
#11839=FACE_BOUND('',#10724,.T.);
#11840=FACE_BOUND('',#10725,.T.);
#11841=FACE_BOUND('',#10726,.T.);
#11842=FACE_BOUND('',#10727,.T.);
#11843=FACE_BOUND('',#10728,.T.);
#11844=FACE_BOUND('',#10729,.T.);
#11845=FACE_BOUND('',#10730,.T.);
#11846=FACE_BOUND('',#10731,.T.);
#11847=FACE_BOUND('',#10732,.T.);
#11848=FACE_BOUND('',#10733,.T.);
#11849=FACE_BOUND('',#10734,.T.);
#11850=FACE_BOUND('',#10735,.T.);
#11851=FACE_BOUND('',#10736,.T.);
#11852=FACE_BOUND('',#10737,.T.);
#11853=FACE_BOUND('',#10738,.T.);
#11854=FACE_BOUND('',#10739,.T.);
#11855=FACE_BOUND('',#10740,.T.);
#11856=FACE_BOUND('',#10741,.T.);
#11857=FACE_BOUND('',#10742,.T.);
#11858=FACE_BOUND('',#10743,.T.);
#11859=FACE_BOUND('',#10744,.T.);
#11860=FACE_BOUND('',#10745,.T.);
#11861=FACE_BOUND('',#10746,.T.);
#11862=FACE_BOUND('',#10747,.T.);
#11863=FACE_BOUND('',#10748,.T.);
#11864=FACE_BOUND('',#10749,.T.);
#11865=FACE_BOUND('',#10750,.T.);
#11866=FACE_BOUND('',#10751,.T.);
#11867=FACE_BOUND('',#10752,.T.);
#11868=FACE_BOUND('',#10753,.T.);
#11869=FACE_BOUND('',#10754,.T.);
#12675=(
BOUNDED_SURFACE()
B_SPLINE_SURFACE(1,2,((#31067,#31068,#31069,#31070,#31071,#31072,#31073,
#31074,#31075,#31076,#31077,#31078,#31079,#31080,#31081,#31082,#31083,#31084,
#31085,#31086,#31087,#31088,#31089,#31090,#31091,#31092,#31093,#31094,#31095,
#31096,#31097,#31098,#31099,#31100,#31101),(#31102,#31103,#31104,#31105,
#31106,#31107,#31108,#31109,#31110,#31111,#31112,#31113,#31114,#31115,#31116,
#31117,#31118,#31119,#31120,#31121,#31122,#31123,#31124,#31125,#31126,#31127,
#31128,#31129,#31130,#31131,#31132,#31133,#31134,#31135,#31136)),
 .RULED_SURF.,.F.,.F.,.F.)
B_SPLINE_SURFACE_WITH_KNOTS((2,2),(3,2,2,2,2,2,2,2,2,2,2,2,2,2,2,2,2,3),
(0.,1.),(0.,0.05,0.1,0.15,0.2,0.25,0.3,0.35,0.4,0.45,0.5,0.55,0.6,0.65,
0.7,0.75,0.8,0.826757087433802),.UNSPECIFIED.)
GEOMETRIC_REPRESENTATION_ITEM()
RATIONAL_B_SPLINE_SURFACE(((1.,0.951056516295154,1.,0.951056516295154,1.,
0.951056516295154,1.,0.951056516295154,1.,0.951056516295154,1.,0.951056516295154,
1.,0.951056516295154,1.,0.951056516295154,1.,0.951056516295154,1.,0.951056516295154,
1.,0.951056516295154,1.,0.951056516295154,1.,0.951056516295154,1.,0.951056516295154,
1.,0.951056516295154,1.,0.951056516295154,1.,0.973808298543891,0.975649142923828),
(1.,0.951056516295154,1.,0.951056516295154,1.,0.951056516295154,1.,0.951056516295154,
1.,0.951056516295154,1.,0.951056516295154,1.,0.951056516295154,1.,0.951056516295154,
1.,0.951056516295154,1.,0.951056516295154,1.,0.951056516295154,1.,0.951056516295154,
1.,0.951056516295154,1.,0.951056516295154,1.,0.951056516295154,1.,0.951056516295154,
1.,0.973808298543891,0.975649142923828)))
REPRESENTATION_ITEM('')
SURFACE()
);
#12829=ADVANCED_FACE('',(#11760),#1578,.T.);
#12830=ADVANCED_FACE('',(#11761),#271,.T.);
#12831=ADVANCED_FACE('',(#11762),#272,.T.);
#12832=ADVANCED_FACE('',(#11763),#273,.T.);
#12833=ADVANCED_FACE('',(#11764),#1579,.F.);
#12834=ADVANCED_FACE('',(#11765),#1580,.T.);
#12835=ADVANCED_FACE('',(#11766),#1581,.F.);
#12836=ADVANCED_FACE('',(#11767),#274,.T.);
#12837=ADVANCED_FACE('',(#11768),#275,.T.);
#12838=ADVANCED_FACE('',(#11769),#276,.T.);
#12839=ADVANCED_FACE('',(#11770),#277,.T.);
#12840=ADVANCED_FACE('',(#11771),#1582,.T.);
#12841=ADVANCED_FACE('',(#11772),#1583,.F.);
#12842=ADVANCED_FACE('',(#11773),#1584,.T.);
#12843=ADVANCED_FACE('',(#11774),#278,.T.);
#12844=ADVANCED_FACE('',(#11775),#1585,.F.);
#12845=ADVANCED_FACE('',(#11776),#1586,.T.);
#12846=ADVANCED_FACE('',(#11777),#279,.T.);
#12847=ADVANCED_FACE('',(#11778),#280,.T.);
#12848=ADVANCED_FACE('',(#11779),#281,.T.);
#12849=ADVANCED_FACE('',(#11780),#282,.T.);
#12850=ADVANCED_FACE('',(#11781),#283,.T.);
#12851=ADVANCED_FACE('',(#11782),#1587,.T.);
#12852=ADVANCED_FACE('',(#11783),#1588,.F.);
#12853=ADVANCED_FACE('',(#11784),#284,.T.);
#12854=ADVANCED_FACE('',(#11785),#1589,.T.);
#12855=ADVANCED_FACE('',(#11786),#1590,.F.);
#12856=ADVANCED_FACE('',(#11787),#285,.T.);
#12857=ADVANCED_FACE('',(#11788),#286,.T.);
#12858=ADVANCED_FACE('',(#11789),#287,.T.);
#12859=ADVANCED_FACE('',(#11790),#288,.T.);
#12860=ADVANCED_FACE('',(#11791),#289,.T.);
#12861=ADVANCED_FACE('',(#11792),#290,.T.);
#12862=ADVANCED_FACE('',(#11793),#1591,.F.);
#12863=ADVANCED_FACE('',(#11794),#1592,.T.);
#12864=ADVANCED_FACE('',(#11795),#291,.T.);
#12865=ADVANCED_FACE('',(#11796),#1593,.F.);
#12866=ADVANCED_FACE('',(#11797),#1594,.T.);
#12867=ADVANCED_FACE('',(#11798),#292,.T.);
#12868=ADVANCED_FACE('',(#11799),#293,.T.);
#12869=ADVANCED_FACE('',(#11800),#294,.T.);
#12870=ADVANCED_FACE('',(#11801),#295,.T.);
#12871=ADVANCED_FACE('',(#11802),#1595,.T.);
#12872=ADVANCED_FACE('',(#11803),#1596,.F.);
#12873=ADVANCED_FACE('',(#11804),#296,.T.);
#12874=ADVANCED_FACE('',(#11805),#1597,.T.);
#12875=ADVANCED_FACE('',(#11806),#1598,.F.);
#12876=ADVANCED_FACE('',(#11807),#297,.T.);
#12877=ADVANCED_FACE('',(#11808),#298,.T.);
#12878=ADVANCED_FACE('',(#11809),#299,.T.);
#12879=ADVANCED_FACE('',(#11810),#300,.T.);
#12880=ADVANCED_FACE('',(#11811),#301,.T.);
#12881=ADVANCED_FACE('',(#11812),#1599,.F.);
#12882=ADVANCED_FACE('',(#11813),#1600,.T.);
#12883=ADVANCED_FACE('',(#11814),#302,.T.);
#12884=ADVANCED_FACE('',(#11815,#11816),#1242,.F.);
#12885=ADVANCED_FACE('',(#11817,#11818),#1243,.F.);
#12886=ADVANCED_FACE('',(#11819,#11820),#1244,.F.);
#12887=ADVANCED_FACE('',(#11821),#12675,.T.);
#12888=ADVANCED_FACE('',(#11822),#53,.T.);
#12889=ADVANCED_FACE('',(#11823),#1601,.F.);
#12890=ADVANCED_FACE('',(#11824),#1245,.T.);
#12891=ADVANCED_FACE('',(#11825),#1246,.F.);
#12892=ADVANCED_FACE('',(#11826,#11827),#1247,.F.);
#12893=ADVANCED_FACE('',(#11828,#11829,#11830,#11831,#11832),#1248,.T.);
#12894=ADVANCED_FACE('',(#11833),#1602,.T.);
#12895=ADVANCED_FACE('',(#11834),#1249,.F.);
#12896=ADVANCED_FACE('',(#11835),#1603,.T.);
#12897=ADVANCED_FACE('',(#11836),#1250,.T.);
#12898=ADVANCED_FACE('',(#11837),#1604,.T.);
#12899=ADVANCED_FACE('',(#11838),#1251,.F.);
#12900=ADVANCED_FACE('',(#11839),#1252,.T.);
#12901=ADVANCED_FACE('',(#11840),#1605,.T.);
#12902=ADVANCED_FACE('',(#11841),#1253,.F.);
#12903=ADVANCED_FACE('',(#11842),#1606,.T.);
#12904=ADVANCED_FACE('',(#11843),#1254,.T.);
#12905=ADVANCED_FACE('',(#11844,#11845,#11846,#11847,#11848),#1255,.F.);
#12906=ADVANCED_FACE('',(#11849,#11850),#1607,.F.);
#12907=ADVANCED_FACE('',(#11851),#1608,.T.);
#12908=ADVANCED_FACE('',(#11852,#11853),#1609,.F.);
#12909=ADVANCED_FACE('',(#11854,#11855),#1610,.F.);
#12910=ADVANCED_FACE('',(#11856,#11857),#1611,.F.);
#12911=ADVANCED_FACE('',(#11858,#11859),#1612,.F.);
#12912=ADVANCED_FACE('',(#11860,#11861),#1613,.F.);
#12913=ADVANCED_FACE('',(#11862,#11863),#1614,.F.);
#12914=ADVANCED_FACE('',(#11864),#303,.T.);
#12915=ADVANCED_FACE('',(#11865),#304,.T.);
#12916=ADVANCED_FACE('',(#11866,#11867),#305,.F.);
#12917=ADVANCED_FACE('',(#11868,#11869),#306,.T.);
#13507=CLOSED_SHELL('',(#12829,#12830,#12831,#12832,#12833,#12834,#12835,
#12836,#12837,#12838,#12839,#12840,#12841,#12842,#12843,#12844,#12845,#12846,
#12847,#12848,#12849,#12850,#12851,#12852,#12853,#12854,#12855,#12856,#12857,
#12858,#12859,#12860,#12861,#12862,#12863,#12864,#12865,#12866,#12867,#12868,
#12869,#12870,#12871,#12872,#12873,#12874,#12875,#12876,#12877,#12878,#12879,
#12880,#12881,#12882,#12883,#12884,#12885,#12886,#12887,#12888,#12889,#12890,
#12891,#12892,#12893,#12894,#12895,#12896,#12897,#12898,#12899,#12900,#12901,
#12902,#12903,#12904,#12905,#12906,#12907,#12908,#12909,#12910,#12911,#12912,
#12913,#12914,#12915,#12916,#12917));
#13534=STYLED_ITEM('',(#13561),#13724);
#13561=PRESENTATION_STYLE_ASSIGNMENT((#13588));
#13588=SURFACE_STYLE_USAGE(.BOTH.,#13615);
#13615=SURFACE_SIDE_STYLE('',(#13642));
#13642=SURFACE_STYLE_FILL_AREA(#13669);
#13669=FILL_AREA_STYLE('',(#13696));
#13696=FILL_AREA_STYLE_COLOUR('',#60);
#13724=MANIFOLD_SOLID_BREP('floating_ring_bottom_connector',#13507);
#13752=SHAPE_DEFINITION_REPRESENTATION(#45534,#13780);
#13780=SHAPE_REPRESENTATION('floating_ring_bottom_connector',(#13802),#45470);
#13802=AXIS2_PLACEMENT_3D('',#19109,#15295,#15296);
#14009=AXIS2_PLACEMENT_3D('',#30741,#15757,#15758);
#14010=AXIS2_PLACEMENT_3D('',#30742,#15759,#15760);
#14011=AXIS2_PLACEMENT_3D('',#30754,#15763,#15764);
#14012=AXIS2_PLACEMENT_3D('',#30755,#15765,#15766);
#14013=AXIS2_PLACEMENT_3D('',#30758,#15767,#15768);
#14014=AXIS2_PLACEMENT_3D('',#30759,#15769,#15770);
#14015=AXIS2_PLACEMENT_3D('',#30760,#15771,#15772);
#14016=AXIS2_PLACEMENT_3D('',#30761,#15773,#15774);
#14017=AXIS2_PLACEMENT_3D('',#30764,#15775,#15776);
#14018=AXIS2_PLACEMENT_3D('',#30765,#15777,#15778);
#14019=AXIS2_PLACEMENT_3D('',#30766,#15779,#15780);
#14020=AXIS2_PLACEMENT_3D('',#30767,#15781,#15782);
#14021=AXIS2_PLACEMENT_3D('',#30770,#15783,#15784);
#14022=AXIS2_PLACEMENT_3D('',#30771,#15785,#15786);
#14023=AXIS2_PLACEMENT_3D('',#30772,#15787,#15788);
#14024=AXIS2_PLACEMENT_3D('',#30773,#15789,#15790);
#14025=AXIS2_PLACEMENT_3D('',#30778,#15793,#15794);
#14026=AXIS2_PLACEMENT_3D('',#30779,#15795,#15796);
#14027=AXIS2_PLACEMENT_3D('',#30784,#15799,#15800);
#14028=AXIS2_PLACEMENT_3D('',#30785,#15801,#15802);
#14029=AXIS2_PLACEMENT_3D('',#30790,#15805,#15806);
#14030=AXIS2_PLACEMENT_3D('',#30791,#15807,#15808);
#14031=AXIS2_PLACEMENT_3D('',#30794,#15809,#15810);
#14032=AXIS2_PLACEMENT_3D('',#30795,#15811,#15812);
#14033=AXIS2_PLACEMENT_3D('',#30796,#15813,#15814);
#14034=AXIS2_PLACEMENT_3D('',#30797,#15815,#15816);
#14035=AXIS2_PLACEMENT_3D('',#30800,#15817,#15818);
#14036=AXIS2_PLACEMENT_3D('',#30802,#15819,#15820);
#14037=AXIS2_PLACEMENT_3D('',#30804,#15821,#15822);
#14038=AXIS2_PLACEMENT_3D('',#30805,#15823,#15824);
#14039=AXIS2_PLACEMENT_3D('',#30806,#15825,#15826);
#14040=AXIS2_PLACEMENT_3D('',#30809,#15827,#15828);
#14041=AXIS2_PLACEMENT_3D('',#30810,#15829,#15830);
#14042=AXIS2_PLACEMENT_3D('',#30811,#15831,#15832);
#14043=AXIS2_PLACEMENT_3D('',#30812,#15833,#15834);
#14044=AXIS2_PLACEMENT_3D('',#30815,#15835,#15836);
#14045=AXIS2_PLACEMENT_3D('',#30816,#15837,#15838);
#14046=AXIS2_PLACEMENT_3D('',#30817,#15839,#15840);
#14047=AXIS2_PLACEMENT_3D('',#30827,#15843,#15844);
#14048=AXIS2_PLACEMENT_3D('',#30828,#15845,#15846);
#14049=AXIS2_PLACEMENT_3D('',#30833,#15849,#15850);
#14050=AXIS2_PLACEMENT_3D('',#30834,#15851,#15852);
#14051=AXIS2_PLACEMENT_3D('',#30839,#15855,#15856);
#14052=AXIS2_PLACEMENT_3D('',#30840,#15857,#15858);
#14053=AXIS2_PLACEMENT_3D('',#30843,#15859,#15860);
#14054=AXIS2_PLACEMENT_3D('',#30844,#15861,#15862);
#14055=AXIS2_PLACEMENT_3D('',#30845,#15863,#15864);
#14056=AXIS2_PLACEMENT_3D('',#30846,#15865,#15866);
#14057=AXIS2_PLACEMENT_3D('',#30851,#15869,#15870);
#14058=AXIS2_PLACEMENT_3D('',#30852,#15871,#15872);
#14059=AXIS2_PLACEMENT_3D('',#30856,#15875,#15876);
#14060=AXIS2_PLACEMENT_3D('',#30857,#15877,#15878);
#14061=AXIS2_PLACEMENT_3D('',#30858,#15879,#15880);
#14062=AXIS2_PLACEMENT_3D('',#30859,#15881,#15882);
#14063=AXIS2_PLACEMENT_3D('',#30860,#15883,#15884);
#14064=AXIS2_PLACEMENT_3D('',#30863,#15885,#15886);
#14065=AXIS2_PLACEMENT_3D('',#30864,#15887,#15888);
#14066=AXIS2_PLACEMENT_3D('',#30865,#15889,#15890);
#14067=AXIS2_PLACEMENT_3D('',#30866,#15891,#15892);
#14068=AXIS2_PLACEMENT_3D('',#30869,#15893,#15894);
#14069=AXIS2_PLACEMENT_3D('',#30870,#15895,#15896);
#14070=AXIS2_PLACEMENT_3D('',#30871,#15897,#15898);
#14071=AXIS2_PLACEMENT_3D('',#30872,#15899,#15900);
#14072=AXIS2_PLACEMENT_3D('',#30875,#15901,#15902);
#14073=AXIS2_PLACEMENT_3D('',#30876,#15903,#15904);
#14074=AXIS2_PLACEMENT_3D('',#30877,#15905,#15906);
#14075=AXIS2_PLACEMENT_3D('',#30878,#15907,#15908);
#14076=AXIS2_PLACEMENT_3D('',#30880,#15909,#15910);
#14077=AXIS2_PLACEMENT_3D('',#30881,#15911,#15912);
#14078=AXIS2_PLACEMENT_3D('',#30882,#15913,#15914);
#14079=AXIS2_PLACEMENT_3D('',#30887,#15917,#15918);
#14080=AXIS2_PLACEMENT_3D('',#30888,#15919,#15920);
#14081=AXIS2_PLACEMENT_3D('',#30892,#15923,#15924);
#14082=AXIS2_PLACEMENT_3D('',#30893,#15925,#15926);
#14083=AXIS2_PLACEMENT_3D('',#30896,#15927,#15928);
#14084=AXIS2_PLACEMENT_3D('',#30897,#15929,#15930);
#14085=AXIS2_PLACEMENT_3D('',#30898,#15931,#15932);
#14086=AXIS2_PLACEMENT_3D('',#30899,#15933,#15934);
#14087=AXIS2_PLACEMENT_3D('',#30904,#15937,#15938);
#14088=AXIS2_PLACEMENT_3D('',#30905,#15939,#15940);
#14089=AXIS2_PLACEMENT_3D('',#30910,#15943,#15944);
#14090=AXIS2_PLACEMENT_3D('',#30911,#15945,#15946);
#14091=AXIS2_PLACEMENT_3D('',#30913,#15947,#15948);
#14092=AXIS2_PLACEMENT_3D('',#30914,#15949,#15950);
#14093=AXIS2_PLACEMENT_3D('',#30915,#15951,#15952);
#14094=AXIS2_PLACEMENT_3D('',#30916,#15953,#15954);
#14095=AXIS2_PLACEMENT_3D('',#30918,#15955,#15956);
#14096=AXIS2_PLACEMENT_3D('',#30919,#15957,#15958);
#14097=AXIS2_PLACEMENT_3D('',#30920,#15959,#15960);
#14098=AXIS2_PLACEMENT_3D('',#30923,#15961,#15962);
#14099=AXIS2_PLACEMENT_3D('',#30924,#15963,#15964);
#14100=AXIS2_PLACEMENT_3D('',#30925,#15965,#15966);
#14101=AXIS2_PLACEMENT_3D('',#30926,#15967,#15968);
#14102=AXIS2_PLACEMENT_3D('',#30929,#15969,#15970);
#14103=AXIS2_PLACEMENT_3D('',#30930,#15971,#15972);
#14104=AXIS2_PLACEMENT_3D('',#30931,#15973,#15974);
#14105=AXIS2_PLACEMENT_3D('',#30932,#15975,#15976);
#14106=AXIS2_PLACEMENT_3D('',#30934,#15977,#15978);
#14107=AXIS2_PLACEMENT_3D('',#30935,#15979,#15980);
#14108=AXIS2_PLACEMENT_3D('',#30936,#15981,#15982);
#14109=AXIS2_PLACEMENT_3D('',#30939,#15983,#15984);
#14110=AXIS2_PLACEMENT_3D('',#30940,#15985,#15986);
#14111=AXIS2_PLACEMENT_3D('',#30941,#15987,#15988);
#14112=AXIS2_PLACEMENT_3D('',#30942,#15989,#15990);
#14113=AXIS2_PLACEMENT_3D('',#30946,#15993,#15994);
#14114=AXIS2_PLACEMENT_3D('',#30947,#15995,#15996);
#14115=AXIS2_PLACEMENT_3D('',#30952,#15999,#16000);
#14116=AXIS2_PLACEMENT_3D('',#30953,#16001,#16002);
#14117=AXIS2_PLACEMENT_3D('',#30956,#16003,#16004);
#14118=AXIS2_PLACEMENT_3D('',#30957,#16005,#16006);
#14119=AXIS2_PLACEMENT_3D('',#30958,#16007,#16008);
#14120=AXIS2_PLACEMENT_3D('',#30959,#16009,#16010);
#14121=AXIS2_PLACEMENT_3D('',#30964,#16013,#16014);
#14122=AXIS2_PLACEMENT_3D('',#30965,#16015,#16016);
#14123=AXIS2_PLACEMENT_3D('',#30969,#16019,#16020);
#14124=AXIS2_PLACEMENT_3D('',#30970,#16021,#16022);
#14125=AXIS2_PLACEMENT_3D('',#30972,#16023,#16024);
#14126=AXIS2_PLACEMENT_3D('',#30973,#16025,#16026);
#14127=AXIS2_PLACEMENT_3D('',#30974,#16027,#16028);
#14128=AXIS2_PLACEMENT_3D('',#30977,#16029,#16030);
#14129=AXIS2_PLACEMENT_3D('',#30978,#16031,#16032);
#14130=AXIS2_PLACEMENT_3D('',#30979,#16033,#16034);
#14131=AXIS2_PLACEMENT_3D('',#30980,#16035,#16036);
#14132=AXIS2_PLACEMENT_3D('',#30983,#16037,#16038);
#14133=AXIS2_PLACEMENT_3D('',#30984,#16039,#16040);
#14134=AXIS2_PLACEMENT_3D('',#30985,#16041,#16042);
#14135=AXIS2_PLACEMENT_3D('',#30986,#16043,#16044);
#14136=AXIS2_PLACEMENT_3D('',#30988,#16045,#16046);
#14137=AXIS2_PLACEMENT_3D('',#30989,#16047,#16048);
#14138=AXIS2_PLACEMENT_3D('',#30990,#16049,#16050);
#14139=AXIS2_PLACEMENT_3D('',#30995,#16053,#16054);
#14140=AXIS2_PLACEMENT_3D('',#30996,#16055,#16056);
#14141=AXIS2_PLACEMENT_3D('',#31000,#16059,#16060);
#14142=AXIS2_PLACEMENT_3D('',#31001,#16061,#16062);
#14143=AXIS2_PLACEMENT_3D('',#31004,#16063,#16064);
#14144=AXIS2_PLACEMENT_3D('',#31005,#16065,#16066);
#14145=AXIS2_PLACEMENT_3D('',#31006,#16067,#16068);
#14146=AXIS2_PLACEMENT_3D('',#31007,#16069,#16070);
#14147=AXIS2_PLACEMENT_3D('',#31012,#16073,#16074);
#14148=AXIS2_PLACEMENT_3D('',#31013,#16075,#16076);
#14149=AXIS2_PLACEMENT_3D('',#31018,#16079,#16080);
#14150=AXIS2_PLACEMENT_3D('',#31019,#16081,#16082);
#14151=AXIS2_PLACEMENT_3D('',#31021,#16083,#16084);
#14152=AXIS2_PLACEMENT_3D('',#31022,#16085,#16086);
#14153=AXIS2_PLACEMENT_3D('',#31023,#16087,#16088);
#14154=AXIS2_PLACEMENT_3D('',#31024,#16089,#16090);
#14155=AXIS2_PLACEMENT_3D('',#31026,#16091,#16092);
#14156=AXIS2_PLACEMENT_3D('',#31027,#16093,#16094);
#14157=AXIS2_PLACEMENT_3D('',#31028,#16095,#16096);
#14158=AXIS2_PLACEMENT_3D('',#31029,#16097,#16098);
#14159=AXIS2_PLACEMENT_3D('',#31030,#16099,#16100);
#14160=AXIS2_PLACEMENT_3D('',#31031,#16101,#16102);
#14161=AXIS2_PLACEMENT_3D('',#31033,#16103,#16104);
#14162=AXIS2_PLACEMENT_3D('',#31034,#16105,#16106);
#14163=AXIS2_PLACEMENT_3D('',#31035,#16107,#16108);
#14164=AXIS2_PLACEMENT_3D('',#31038,#16109,#16110);
#14165=AXIS2_PLACEMENT_3D('',#31039,#16111,#16112);
#14166=AXIS2_PLACEMENT_3D('',#31040,#16113,#16114);
#14167=AXIS2_PLACEMENT_3D('',#31041,#16115,#16116);
#14168=AXIS2_PLACEMENT_3D('',#31045,#16119,#16120);
#14169=AXIS2_PLACEMENT_3D('',#31046,#16121,#16122);
#14170=AXIS2_PLACEMENT_3D('',#31050,#16125,#16126);
#14171=AXIS2_PLACEMENT_3D('',#31051,#16127,#16128);
#14172=AXIS2_PLACEMENT_3D('',#31052,#16129,#16130);
#14173=AXIS2_PLACEMENT_3D('',#31053,#16131,#16132);
#14174=AXIS2_PLACEMENT_3D('',#31055,#16133,#16134);
#14175=AXIS2_PLACEMENT_3D('',#31057,#16135,#16136);
#14176=AXIS2_PLACEMENT_3D('',#31058,#16137,#16138);
#14177=AXIS2_PLACEMENT_3D('',#31060,#16139,#16140);
#14178=AXIS2_PLACEMENT_3D('',#31062,#16141,#16142);
#14179=AXIS2_PLACEMENT_3D('',#31063,#16143,#16144);
#14180=AXIS2_PLACEMENT_3D('',#31065,#16145,#16146);
#14181=AXIS2_PLACEMENT_3D('',#31533,#16151,#16152);
#14182=AXIS2_PLACEMENT_3D('',#31536,#16155,#16156);
#14183=AXIS2_PLACEMENT_3D('',#31538,#16158,#16159);
#14184=AXIS2_PLACEMENT_3D('',#31540,#16161,#16162);
#14185=AXIS2_PLACEMENT_3D('',#31541,#16163,#16164);
#14186=AXIS2_PLACEMENT_3D('',#31543,#16165,#16166);
#14187=AXIS2_PLACEMENT_3D('',#31545,#16167,#16168);
#14188=AXIS2_PLACEMENT_3D('',#31546,#16169,#16170);
#14189=AXIS2_PLACEMENT_3D('',#31548,#16171,#16172);
#14190=AXIS2_PLACEMENT_3D('',#31550,#16173,#16174);
#14191=AXIS2_PLACEMENT_3D('',#31552,#16175,#16176);
#14192=AXIS2_PLACEMENT_3D('',#31553,#16177,#16178);
#14193=AXIS2_PLACEMENT_3D('',#31555,#16179,#16180);
#14194=AXIS2_PLACEMENT_3D('',#31556,#16181,#16182);
#14195=AXIS2_PLACEMENT_3D('',#31557,#16183,#16184);
#14196=AXIS2_PLACEMENT_3D('',#31558,#16185,#16186);
#14197=AXIS2_PLACEMENT_3D('',#31559,#16187,#16188);
#14198=AXIS2_PLACEMENT_3D('',#31560,#16189,#16190);
#14199=AXIS2_PLACEMENT_3D('',#31562,#16192,#16193);
#14200=AXIS2_PLACEMENT_3D('',#31563,#16194,#16195);
#14201=AXIS2_PLACEMENT_3D('',#31564,#16196,#16197);
#14202=AXIS2_PLACEMENT_3D('',#31565,#16198,#16199);
#14203=AXIS2_PLACEMENT_3D('',#31566,#16200,#16201);
#14204=AXIS2_PLACEMENT_3D('',#31567,#16202,#16203);
#14205=AXIS2_PLACEMENT_3D('',#31568,#16204,#16205);
#14206=AXIS2_PLACEMENT_3D('',#31569,#16206,#16207);
#14207=AXIS2_PLACEMENT_3D('',#31570,#16208,#16209);
#14208=AXIS2_PLACEMENT_3D('',#31571,#16210,#16211);
#14209=AXIS2_PLACEMENT_3D('',#31573,#16212,#16213);
#14210=AXIS2_PLACEMENT_3D('',#31575,#16214,#16215);
#14211=AXIS2_PLACEMENT_3D('',#31577,#16216,#16217);
#14212=AXIS2_PLACEMENT_3D('',#31578,#16218,#16219);
#14213=AXIS2_PLACEMENT_3D('',#31579,#16220,#16221);
#14214=AXIS2_PLACEMENT_3D('',#31580,#16222,#16223);
#14215=AXIS2_PLACEMENT_3D('',#31581,#16224,#16225);
#14216=AXIS2_PLACEMENT_3D('',#31582,#16226,#16227);
#14217=AXIS2_PLACEMENT_3D('',#31583,#16228,#16229);
#14218=AXIS2_PLACEMENT_3D('',#31584,#16230,#16231);
#14219=AXIS2_PLACEMENT_3D('',#31585,#16232,#16233);
#14220=AXIS2_PLACEMENT_3D('',#31586,#16234,#16235);
#14221=AXIS2_PLACEMENT_3D('',#31587,#16236,#16237);
#14222=AXIS2_PLACEMENT_3D('',#31588,#16238,#16239);
#14223=AXIS2_PLACEMENT_3D('',#31589,#16240,#16241);
#14224=AXIS2_PLACEMENT_3D('',#31591,#16242,#16243);
#15295=DIRECTION('',(0.,0.,1.));
#15296=DIRECTION('',(1.,0.,0.));
#15757=DIRECTION('',(0.891006524188365,0.453990499739553,0.));
#15758=DIRECTION('',(-0.453990499739553,0.891006524188365,0.));
#15759=DIRECTION('',(0.891006524188366,0.453990499739551,0.));
#15760=DIRECTION('',(0.45399049973955,-0.891006524188366,0.));
#15761=DIRECTION('',(-0.891006524188365,-0.453990499739553,0.));
#15762=DIRECTION('',(0.891006524188365,0.453990499739553,0.));
#15763=DIRECTION('',(0.,0.,-1.));
#15764=DIRECTION('',(-1.,0.,0.));
#15765=DIRECTION('',(-0.966706191517614,-0.255888919809962,-2.46545352372542E-17));
#15766=DIRECTION('',(-0.255888919809963,0.966706191517614,0.));
#15767=DIRECTION('',(0.,0.,1.));
#15768=DIRECTION('',(-1.,0.,0.));
#15769=DIRECTION('',(0.,0.,-1.));
#15770=DIRECTION('',(-1.,0.,0.));
#15771=DIRECTION('',(0.,0.,-1.));
#15772=DIRECTION('',(-1.,0.,0.));
#15773=DIRECTION('',(0.86760952952486,0.497246120424937,0.));
#15774=DIRECTION('',(-0.497246120424937,0.86760952952486,0.));
#15775=DIRECTION('',(0.,0.,-1.));
#15776=DIRECTION('',(-1.,0.,0.));
#15777=DIRECTION('',(0.,0.,1.));
#15778=DIRECTION('',(-1.,-3.46944695195361E-15,0.));
#15779=DIRECTION('',(0.,0.,-1.));
#15780=DIRECTION('',(-1.,0.,0.));
#15781=DIRECTION('',(-0.891006524188365,0.453990499739553,0.));
#15782=DIRECTION('',(-0.453990499739553,-0.891006524188365,0.));
#15783=DIRECTION('',(0.,0.,1.));
#15784=DIRECTION('',(-1.,-1.73472347597681E-15,0.));
#15785=DIRECTION('',(0.,0.,-1.));
#15786=DIRECTION('',(-1.,0.,0.));
#15787=DIRECTION('',(0.,0.,1.));
#15788=DIRECTION('',(1.,0.,0.));
#15789=DIRECTION('',(0.,0.,1.));
#15790=DIRECTION('',(-1.,-3.46944695195361E-15,0.));
#15791=DIRECTION('',(0.,0.,1.));
#15792=DIRECTION('',(0.,0.,-1.));
#15793=DIRECTION('',(0.891006524188365,-0.453990499739553,0.));
#15794=DIRECTION('',(0.453990499739554,0.891006524188364,0.));
#15795=DIRECTION('',(-0.891006524188365,0.453990499739553,0.));
#15796=DIRECTION('',(0.453990499739553,0.891006524188365,0.));
#15797=DIRECTION('',(0.891006524188365,-0.453990499739553,0.));
#15798=DIRECTION('',(-0.891006524188365,0.453990499739553,0.));
#15799=DIRECTION('',(0.,0.,1.));
#15800=DIRECTION('',(1.,0.,0.));
#15801=DIRECTION('',(0.,0.,1.));
#15802=DIRECTION('',(-1.,-1.73472347597681E-15,0.));
#15803=DIRECTION('',(0.,0.,1.));
#15804=DIRECTION('',(0.,0.,-1.));
#15805=DIRECTION('',(0.,0.,-1.));
#15806=DIRECTION('',(-1.,0.,0.));
#15807=DIRECTION('',(0.,0.,1.));
#15808=DIRECTION('',(-1.,2.25514051876985E-14,0.));
#15809=DIRECTION('',(0.86760952952486,0.497246120424937,0.));
#15810=DIRECTION('',(-0.497246120424937,0.86760952952486,0.));
#15811=DIRECTION('',(-0.891006524188365,-0.453990499739553,-1.57509595553729E-15));
#15812=DIRECTION('',(0.453990499739553,-0.891006524188365,0.));
#15813=DIRECTION('',(0.,0.,-1.));
#15814=DIRECTION('',(-1.,0.,0.));
#15815=DIRECTION('',(-0.838670567945428,-0.544639035015021,0.));
#15816=DIRECTION('',(0.544639035015021,-0.838670567945428,0.));
#15817=DIRECTION('',(0.,0.,-1.));
#15818=DIRECTION('',(-1.,0.,0.));
#15819=DIRECTION('',(-0.864432536983703,-0.50274883292149,0.));
#15820=DIRECTION('',(-0.50274883292149,0.864432536983703,0.));
#15821=DIRECTION('',(0.,0.,1.));
#15822=DIRECTION('',(-1.,9.6277152916713E-14,0.));
#15823=DIRECTION('',(0.,0.,-1.));
#15824=DIRECTION('',(-1.,0.,0.));
#15825=DIRECTION('',(-0.867609529524852,0.497246120424951,0.));
#15826=DIRECTION('',(-0.497246120424951,-0.867609529524852,0.));
#15827=DIRECTION('',(0.,0.,1.));
#15828=DIRECTION('',(-1.,-1.90819582357449E-13,0.));
#15829=DIRECTION('',(0.,0.,-1.));
#15830=DIRECTION('',(-1.,0.,0.));
#15831=DIRECTION('',(0.,0.,-1.));
#15832=DIRECTION('',(-1.,0.,0.));
#15833=DIRECTION('',(0.,0.,1.));
#15834=DIRECTION('',(-1.,0.,0.));
#15835=DIRECTION('',(0.966706191517614,0.255888919809962,0.));
#15836=DIRECTION('',(-0.255888919809962,0.966706191517615,0.));
#15837=DIRECTION('',(-0.891006524188365,0.453990499739553,-1.47230103896192E-17));
#15838=DIRECTION('',(-0.453990499739553,-0.891006524188365,0.));
#15839=DIRECTION('',(-0.891006524188365,-0.453990499739553,0.));
#15840=DIRECTION('',(0.453990499739553,-0.891006524188365,0.));
#15841=DIRECTION('',(0.891006524188365,0.453990499739553,0.));
#15842=DIRECTION('',(-0.891006524188365,-0.453990499739553,0.));
#15843=DIRECTION('',(0.,0.,1.));
#15844=DIRECTION('',(1.,0.,0.));
#15845=DIRECTION('',(0.,0.,1.));
#15846=DIRECTION('',(-1.,9.6277152916713E-14,0.));
#15847=DIRECTION('',(0.,0.,1.));
#15848=DIRECTION('',(0.,0.,-1.));
#15849=DIRECTION('',(-0.838670567945428,-0.544639035015021,0.));
#15850=DIRECTION('',(0.544639035015021,-0.838670567945428,0.));
#15851=DIRECTION('',(-0.838670567945428,-0.544639035015022,0.));
#15852=DIRECTION('',(-0.544639035015022,0.838670567945428,0.));
#15853=DIRECTION('',(0.838670567945428,0.544639035015021,0.));
#15854=DIRECTION('',(-0.838670567945428,-0.544639035015021,0.));
#15855=DIRECTION('',(0.,0.,-1.));
#15856=DIRECTION('',(-1.,0.,0.));
#15857=DIRECTION('',(0.86443253698369,-0.50274883292151,0.));
#15858=DIRECTION('',(-0.50274883292151,-0.86443253698369,0.));
#15859=DIRECTION('',(0.,0.,1.));
#15860=DIRECTION('',(-1.,0.,0.));
#15861=DIRECTION('',(0.,0.,-1.));
#15862=DIRECTION('',(-1.,0.,0.));
#15863=DIRECTION('',(0.,0.,1.));
#15864=DIRECTION('',(1.,0.,0.));
#15865=DIRECTION('',(0.,0.,1.));
#15866=DIRECTION('',(-1.,-1.90819582357449E-13,0.));
#15867=DIRECTION('',(0.,0.,1.));
#15868=DIRECTION('',(0.,0.,-1.));
#15869=DIRECTION('',(-0.891006524188365,0.453990499739553,0.));
#15870=DIRECTION('',(-0.453990499739553,-0.891006524188365,0.));
#15871=DIRECTION('',(-0.891006524188365,0.453990499739553,0.));
#15872=DIRECTION('',(0.453990499739553,0.891006524188365,0.));
#15873=DIRECTION('',(0.891006524188365,-0.453990499739553,0.));
#15874=DIRECTION('',(-0.891006524188365,0.453990499739553,0.));
#15875=DIRECTION('',(0.,0.,-1.));
#15876=DIRECTION('',(-1.,0.,0.));
#15877=DIRECTION('',(0.,0.,1.));
#15878=DIRECTION('',(-1.,0.,0.));
#15879=DIRECTION('',(0.,0.,-1.));
#15880=DIRECTION('',(-1.,0.,0.));
#15881=DIRECTION('',(0.,0.,-1.));
#15882=DIRECTION('',(-1.,0.,0.));
#15883=DIRECTION('',(0.,0.,1.));
#15884=DIRECTION('',(-1.,3.90312782094782E-14,0.));
#15885=DIRECTION('',(-0.838670567945428,-0.544639035015021,0.));
#15886=DIRECTION('',(0.544639035015021,-0.838670567945428,0.));
#15887=DIRECTION('',(-0.864432536983703,-0.50274883292149,0.));
#15888=DIRECTION('',(-0.50274883292149,0.864432536983703,0.));
#15889=DIRECTION('',(0.,0.,-1.));
#15890=DIRECTION('',(-1.,0.,0.));
#15891=DIRECTION('',(-0.26174679065642,-0.96513657975494,0.));
#15892=DIRECTION('',(0.96513657975494,-0.26174679065642,0.));
#15893=DIRECTION('',(0.,0.,-1.));
#15894=DIRECTION('',(-1.,0.,0.));
#15895=DIRECTION('',(0.,0.,1.));
#15896=DIRECTION('',(-1.,1.73472347597681E-15,0.));
#15897=DIRECTION('',(0.,0.,-1.));
#15898=DIRECTION('',(-1.,0.,0.));
#15899=DIRECTION('',(0.838670567945428,-0.544639035015021,0.));
#15900=DIRECTION('',(0.544639035015021,0.838670567945428,0.));
#15901=DIRECTION('',(0.,0.,1.));
#15902=DIRECTION('',(-1.,2.51534904016637E-14,0.));
#15903=DIRECTION('',(0.,0.,-1.));
#15904=DIRECTION('',(-1.,0.,0.));
#15905=DIRECTION('',(0.,0.,-1.));
#15906=DIRECTION('',(-1.,0.,0.));
#15907=DIRECTION('',(-0.867609529524852,0.497246120424951,0.));
#15908=DIRECTION('',(-0.497246120424951,-0.867609529524852,0.));
#15909=DIRECTION('',(0.,0.,1.));
#15910=DIRECTION('',(-1.,0.,0.));
#15911=DIRECTION('',(0.838670567945428,0.544639035015021,0.));
#15912=DIRECTION('',(-0.544639035015021,0.838670567945428,0.));
#15913=DIRECTION('',(-0.838670567945428,-0.544639035015022,6.28163167848562E-16));
#15914=DIRECTION('',(-0.544639035015022,0.838670567945428,0.));
#15915=DIRECTION('',(0.838670567945428,0.544639035015021,0.));
#15916=DIRECTION('',(-0.838670567945428,-0.544639035015021,0.));
#15917=DIRECTION('',(0.,0.,1.));
#15918=DIRECTION('',(1.,0.,0.));
#15919=DIRECTION('',(0.,0.,1.));
#15920=DIRECTION('',(-1.,1.73472347597681E-15,0.));
#15921=DIRECTION('',(0.,0.,1.));
#15922=DIRECTION('',(0.,0.,-1.));
#15923=DIRECTION('',(0.,0.,-1.));
#15924=DIRECTION('',(-1.,0.,0.));
#15925=DIRECTION('',(-0.704959400861195,-0.709247659944977,0.));
#15926=DIRECTION('',(-0.709247659944977,0.704959400861195,0.));
#15927=DIRECTION('',(0.,0.,-1.));
#15928=DIRECTION('',(-1.,0.,0.));
#15929=DIRECTION('',(0.,0.,1.));
#15930=DIRECTION('',(-1.,8.88178419700125E-16,0.));
#15931=DIRECTION('',(-0.838670567945428,0.544639035015022,0.));
#15932=DIRECTION('',(-0.544639035015022,-0.838670567945428,0.));
#15933=DIRECTION('',(0.838670567945428,-0.544639035015022,0.));
#15934=DIRECTION('',(-0.544639035015022,-0.838670567945428,0.));
#15935=DIRECTION('',(-0.838670567945428,0.544639035015022,0.));
#15936=DIRECTION('',(0.838670567945428,-0.544639035015022,0.));
#15937=DIRECTION('',(0.,0.,1.));
#15938=DIRECTION('',(1.,0.,0.));
#15939=DIRECTION('',(0.,0.,1.));
#15940=DIRECTION('',(-1.,2.51534904016637E-14,0.));
#15941=DIRECTION('',(0.,0.,1.));
#15942=DIRECTION('',(0.,0.,-1.));
#15943=DIRECTION('',(0.,0.,-1.));
#15944=DIRECTION('',(-1.,0.,0.));
#15945=DIRECTION('',(0.86443253698369,-0.50274883292151,0.));
#15946=DIRECTION('',(-0.50274883292151,-0.86443253698369,0.));
#15947=DIRECTION('',(0.,0.,1.));
#15948=DIRECTION('',(-1.,0.,0.));
#15949=DIRECTION('',(0.,0.,-1.));
#15950=DIRECTION('',(-1.,0.,0.));
#15951=DIRECTION('',(0.,0.,-1.));
#15952=DIRECTION('',(-1.,0.,0.));
#15953=DIRECTION('',(0.,0.,1.));
#15954=DIRECTION('',(-1.,0.,0.));
#15955=DIRECTION('',(-0.26174679065642,-0.96513657975494,0.));
#15956=DIRECTION('',(0.96513657975494,-0.26174679065642,0.));
#15957=DIRECTION('',(0.,0.,-1.));
#15958=DIRECTION('',(-1.,0.,0.));
#15959=DIRECTION('',(-0.0523359562429378,-0.998629534754574,-4.53942059661595E-17));
#15960=DIRECTION('',(0.998629534754574,-0.0523359562429379,0.));
#15961=DIRECTION('',(0.,0.,-1.));
#15962=DIRECTION('',(-1.,0.,0.));
#15963=DIRECTION('',(0.,0.,1.));
#15964=DIRECTION('',(-1.,5.20417042793042E-15,0.));
#15965=DIRECTION('',(0.,0.,-1.));
#15966=DIRECTION('',(-1.,0.,0.));
#15967=DIRECTION('',(0.26174679065642,-0.96513657975494,0.));
#15968=DIRECTION('',(0.96513657975494,0.26174679065642,0.));
#15969=DIRECTION('',(0.,0.,1.));
#15970=DIRECTION('',(-1.,0.,0.));
#15971=DIRECTION('',(0.,0.,-1.));
#15972=DIRECTION('',(-1.,0.,0.));
#15973=DIRECTION('',(0.,0.,-1.));
#15974=DIRECTION('',(-1.,0.,0.));
#15975=DIRECTION('',(0.838670567945428,-0.544639035015021,0.));
#15976=DIRECTION('',(0.544639035015021,0.838670567945428,0.));
#15977=DIRECTION('',(0.,0.,1.));
#15978=DIRECTION('',(-1.,-2.60208521396521E-15,0.));
#15979=DIRECTION('',(0.,0.,-1.));
#15980=DIRECTION('',(-1.,0.,0.));
#15981=DIRECTION('',(-0.704959400861195,-0.709247659944977,0.));
#15982=DIRECTION('',(-0.709247659944977,0.704959400861195,0.));
#15983=DIRECTION('',(0.,0.,-1.));
#15984=DIRECTION('',(-1.,0.,0.));
#15985=DIRECTION('',(0.,0.,1.));
#15986=DIRECTION('',(-1.,1.77635683940025E-15,0.));
#15987=DIRECTION('',(0.,0.,1.));
#15988=DIRECTION('',(1.,0.,0.));
#15989=DIRECTION('',(0.,0.,1.));
#15990=DIRECTION('',(-1.,5.20417042793042E-15,0.));
#15991=DIRECTION('',(0.,0.,1.));
#15992=DIRECTION('',(0.,0.,-1.));
#15993=DIRECTION('',(-0.052335956242937,-0.998629534754574,0.));
#15994=DIRECTION('',(0.998629534754574,-0.052335956242937,0.));
#15995=DIRECTION('',(-0.052335956242936,-0.998629534754574,0.));
#15996=DIRECTION('',(-0.998629534754574,0.0523359562429361,0.));
#15997=DIRECTION('',(0.052335956242937,0.998629534754574,0.));
#15998=DIRECTION('',(-0.052335956242937,-0.998629534754574,0.));
#15999=DIRECTION('',(0.,0.,-1.));
#16000=DIRECTION('',(-1.,0.,0.));
#16001=DIRECTION('',(0.704959400861195,-0.709247659944977,0.));
#16002=DIRECTION('',(-0.709247659944977,-0.704959400861195,0.));
#16003=DIRECTION('',(0.,0.,1.));
#16004=DIRECTION('',(-1.,0.,0.));
#16005=DIRECTION('',(0.,0.,-1.));
#16006=DIRECTION('',(-1.,0.,0.));
#16007=DIRECTION('',(0.,0.,1.));
#16008=DIRECTION('',(1.,0.,0.));
#16009=DIRECTION('',(0.,0.,1.));
#16010=DIRECTION('',(-1.,0.,0.));
#16011=DIRECTION('',(0.,0.,1.));
#16012=DIRECTION('',(0.,0.,-1.));
#16013=DIRECTION('',(0.838670567945428,-0.544639035015022,0.));
#16014=DIRECTION('',(0.544639035015022,0.838670567945428,0.));
#16015=DIRECTION('',(0.838670567945427,-0.544639035015022,0.));
#16016=DIRECTION('',(-0.544639035015022,-0.838670567945428,0.));
#16017=DIRECTION('',(-0.838670567945428,0.544639035015022,0.));
#16018=DIRECTION('',(0.838670567945428,-0.544639035015022,0.));
#16019=DIRECTION('',(0.,0.,-1.));
#16020=DIRECTION('',(-1.,0.,0.));
#16021=DIRECTION('',(0.,0.,1.));
#16022=DIRECTION('',(-1.,1.73472347597681E-15,0.));
#16023=DIRECTION('',(-0.0523359562429378,-0.998629534754574,0.));
#16024=DIRECTION('',(0.998629534754574,-0.0523359562429379,0.));
#16025=DIRECTION('',(0.,0.,-1.));
#16026=DIRECTION('',(-1.,0.,0.));
#16027=DIRECTION('',(-0.00317699254116094,-0.999994953346462,0.));
#16028=DIRECTION('',(0.999994953346462,-0.00317699254116094,0.));
#16029=DIRECTION('',(0.,0.,-1.));
#16030=DIRECTION('',(-1.,0.,0.));
#16031=DIRECTION('',(0.,0.,1.));
#16032=DIRECTION('',(-1.,0.,0.));
#16033=DIRECTION('',(0.,0.,-1.));
#16034=DIRECTION('',(-1.,0.,0.));
#16035=DIRECTION('',(0.0523359562429378,-0.998629534754574,0.));
#16036=DIRECTION('',(0.998629534754574,0.0523359562429378,0.));
#16037=DIRECTION('',(0.,0.,1.));
#16038=DIRECTION('',(-1.,0.,0.));
#16039=DIRECTION('',(0.,0.,-1.));
#16040=DIRECTION('',(-1.,0.,0.));
#16041=DIRECTION('',(0.,0.,-1.));
#16042=DIRECTION('',(-1.,0.,0.));
#16043=DIRECTION('',(0.26174679065642,-0.96513657975494,0.));
#16044=DIRECTION('',(0.96513657975494,0.26174679065642,0.));
#16045=DIRECTION('',(0.,0.,1.));
#16046=DIRECTION('',(-1.,0.,0.));
#16047=DIRECTION('',(0.052335956242937,0.998629534754574,0.));
#16048=DIRECTION('',(-0.998629534754574,0.052335956242937,0.));
#16049=DIRECTION('',(-0.0523359562429361,-0.998629534754574,4.5394205966158E-17));
#16050=DIRECTION('',(-0.998629534754574,0.0523359562429361,0.));
#16051=DIRECTION('',(0.052335956242937,0.998629534754574,0.));
#16052=DIRECTION('',(-0.052335956242937,-0.998629534754574,0.));
#16053=DIRECTION('',(0.,0.,1.));
#16054=DIRECTION('',(1.,0.,0.));
#16055=DIRECTION('',(0.,0.,1.));
#16056=DIRECTION('',(-1.,0.,0.));
#16057=DIRECTION('',(0.,0.,1.));
#16058=DIRECTION('',(0.,0.,-1.));
#16059=DIRECTION('',(0.,0.,-1.));
#16060=DIRECTION('',(-1.,0.,0.));
#16061=DIRECTION('',(-0.00317699254116094,0.999994953346462,0.));
#16062=DIRECTION('',(0.999994953346462,0.00317699254116094,0.));
#16063=DIRECTION('',(0.,0.,-1.));
#16064=DIRECTION('',(-1.,0.,0.));
#16065=DIRECTION('',(0.,0.,1.));
#16066=DIRECTION('',(-1.,0.,0.));
#16067=DIRECTION('',(-0.052335956242937,0.998629534754574,0.));
#16068=DIRECTION('',(-0.998629534754574,-0.052335956242937,0.));
#16069=DIRECTION('',(0.0523359562429361,-0.998629534754574,-4.5394205966158E-17));
#16070=DIRECTION('',(-0.998629534754574,-0.0523359562429361,0.));
#16071=DIRECTION('',(-0.052335956242937,0.998629534754574,0.));
#16072=DIRECTION('',(0.052335956242937,-0.998629534754574,0.));
#16073=DIRECTION('',(0.,0.,1.));
#16074=DIRECTION('',(1.,0.,0.));
#16075=DIRECTION('',(0.,0.,1.));
#16076=DIRECTION('',(-1.,0.,0.));
#16077=DIRECTION('',(0.,0.,1.));
#16078=DIRECTION('',(0.,0.,-1.));
#16079=DIRECTION('',(0.,0.,-1.));
#16080=DIRECTION('',(-1.,0.,0.));
#16081=DIRECTION('',(0.704959400861195,-0.709247659944977,0.));
#16082=DIRECTION('',(-0.709247659944977,-0.704959400861195,0.));
#16083=DIRECTION('',(0.,0.,1.));
#16084=DIRECTION('',(-1.,0.,0.));
#16085=DIRECTION('',(0.,0.,-1.));
#16086=DIRECTION('',(-1.,0.,0.));
#16087=DIRECTION('',(0.,0.,-1.));
#16088=DIRECTION('',(-1.,0.,0.));
#16089=DIRECTION('',(0.,0.,1.));
#16090=DIRECTION('',(-1.,0.,0.));
#16091=DIRECTION('',(-0.00317699254116094,-0.999994953346462,0.));
#16092=DIRECTION('',(0.999994953346462,-0.00317699254116094,0.));
#16093=DIRECTION('',(0.,0.,-1.));
#16094=DIRECTION('',(-1.,0.,0.));
#16095=DIRECTION('',(0.,0.,1.));
#16096=DIRECTION('',(-1.,0.,0.));
#16097=DIRECTION('',(0.,0.,-1.));
#16098=DIRECTION('',(-1.,0.,0.));
#16099=DIRECTION('',(0.,0.,-1.));
#16100=DIRECTION('',(-1.,0.,0.));
#16101=DIRECTION('',(0.0523359562429378,-0.998629534754574,0.));
#16102=DIRECTION('',(0.998629534754574,0.0523359562429378,0.));
#16103=DIRECTION('',(0.,0.,1.));
#16104=DIRECTION('',(-1.,0.,0.));
#16105=DIRECTION('',(0.,0.,-1.));
#16106=DIRECTION('',(-1.,0.,0.));
#16107=DIRECTION('',(-0.00317699254116094,0.999994953346462,0.));
#16108=DIRECTION('',(0.999994953346462,0.00317699254116094,0.));
#16109=DIRECTION('',(0.,0.,-1.));
#16110=DIRECTION('',(-1.,0.,0.));
#16111=DIRECTION('',(0.,0.,1.));
#16112=DIRECTION('',(-1.,0.,0.));
#16113=DIRECTION('',(0.,0.,1.));
#16114=DIRECTION('',(1.,0.,0.));
#16115=DIRECTION('',(0.,0.,1.));
#16116=DIRECTION('',(-1.,0.,0.));
#16117=DIRECTION('',(0.,0.,1.));
#16118=DIRECTION('',(0.,0.,-1.));
#16119=DIRECTION('',(0.052335956242937,-0.998629534754574,0.));
#16120=DIRECTION('',(0.998629534754574,0.052335956242937,0.));
#16121=DIRECTION('',(0.052335956242936,-0.998629534754574,0.));
#16122=DIRECTION('',(-0.998629534754574,-0.0523359562429361,0.));
#16123=DIRECTION('',(-0.052335956242937,0.998629534754574,0.));
#16124=DIRECTION('',(0.052335956242937,-0.998629534754574,0.));
#16125=DIRECTION('',(0.,0.,-1.));
#16126=DIRECTION('',(-1.,0.,0.));
#16127=DIRECTION('',(0.,0.,1.));
#16128=DIRECTION('',(-1.,0.,0.));
#16129=DIRECTION('',(0.,0.,1.));
#16130=DIRECTION('',(1.,0.,0.));
#16131=DIRECTION('',(0.,0.,-1.));
#16132=DIRECTION('',(-1.,0.,0.));
#16133=DIRECTION('',(0.,0.,-1.));
#16134=DIRECTION('',(-1.,0.,0.));
#16135=DIRECTION('',(0.,0.,1.));
#16136=DIRECTION('',(1.,0.,0.));
#16137=DIRECTION('',(0.,0.,-1.));
#16138=DIRECTION('',(-1.,0.,0.));
#16139=DIRECTION('',(0.,0.,-1.));
#16140=DIRECTION('',(-1.,0.,0.));
#16141=DIRECTION('',(0.,0.,1.));
#16142=DIRECTION('',(1.,0.,0.));
#16143=DIRECTION('',(0.,0.,-1.));
#16144=DIRECTION('',(-1.,0.,0.));
#16145=DIRECTION('',(0.,0.,-1.));
#16146=DIRECTION('',(-1.,0.,0.));
#16147=DIRECTION('',(0.866025403784438,0.,-0.5));
#16148=DIRECTION('',(0.493314204695212,-0.711787254343556,0.499999999999992));
#16149=DIRECTION('',(-0.866025403784438,0.,-0.5));
#16150=DIRECTION('',(-0.493317826094965,0.711784843538332,0.499999858966031));
#16151=DIRECTION('',(0.,0.,-1.));
#16152=DIRECTION('',(-1.,0.,0.));
#16153=DIRECTION('',(0.,0.,-1.));
#16154=DIRECTION('',(4.82420265013935E-6,3.34348237489084E-6,0.999999999982774));
#16155=DIRECTION('',(0.821901125801989,0.569630177751691,0.));
#16156=DIRECTION('',(-0.569630177751691,0.821901125801989,0.));
#16157=DIRECTION('',(0.,0.,-1.));
#16158=DIRECTION('',(0.,-1.,0.));
#16159=DIRECTION('',(0.,0.,-1.));
#16160=DIRECTION('',(0.,0.,1.));
#16161=DIRECTION('',(0.,0.,1.));
#16162=DIRECTION('',(1.,0.,0.));
#16163=DIRECTION('',(0.,0.,1.));
#16164=DIRECTION('',(1.,0.,0.));
#16165=DIRECTION('',(0.,0.,-1.));
#16166=DIRECTION('',(1.,0.,0.));
#16167=DIRECTION('',(0.,0.,-1.));
#16168=DIRECTION('',(-1.,0.,0.));
#16169=DIRECTION('',(0.,0.,-1.));
#16170=DIRECTION('',(-1.,0.,0.));
#16171=DIRECTION('',(0.,0.,-1.));
#16172=DIRECTION('',(-1.,0.,0.));
#16173=DIRECTION('',(0.,0.,-1.));
#16174=DIRECTION('',(-1.,0.,0.));
#16175=DIRECTION('',(0.,0.,-1.));
#16176=DIRECTION('',(-1.,0.,0.));
#16177=DIRECTION('',(0.,0.,1.));
#16178=DIRECTION('',(-1.,0.,0.));
#16179=DIRECTION('',(0.,0.,1.));
#16180=DIRECTION('',(1.,0.,0.));
#16181=DIRECTION('',(0.544639035015021,-0.838670567945428,0.));
#16182=DIRECTION('',(0.838670567945428,0.544639035015021,0.));
#16183=DIRECTION('',(0.,0.,1.));
#16184=DIRECTION('',(1.,0.,0.));
#16185=DIRECTION('',(0.,0.,1.));
#16186=DIRECTION('',(-1.,0.,0.));
#16187=DIRECTION('',(0.,0.,-1.));
#16188=DIRECTION('',(-1.,0.,0.));
#16189=DIRECTION('',(0.453990499739553,-0.891006524188365,0.));
#16190=DIRECTION('',(0.891006524188365,0.453990499739553,0.));
#16191=DIRECTION('',(0.,0.,1.));
#16192=DIRECTION('',(0.,0.,1.));
#16193=DIRECTION('',(1.,0.,0.));
#16194=DIRECTION('',(0.453990499739553,0.891006524188365,0.));
#16195=DIRECTION('',(-0.891006524188365,0.453990499739553,0.));
#16196=DIRECTION('',(0.544639035015022,0.838670567945428,0.));
#16197=DIRECTION('',(-0.838670567945428,0.544639035015022,0.));
#16198=DIRECTION('',(0.,0.,1.));
#16199=DIRECTION('',(1.,0.,0.));
#16200=DIRECTION('',(-0.998629534754574,-0.052335956242937,0.));
#16201=DIRECTION('',(0.052335956242937,-0.998629534754574,0.));
#16202=DIRECTION('',(0.,0.,1.));
#16203=DIRECTION('',(1.,0.,0.));
#16204=DIRECTION('',(-0.998629534754574,0.052335956242937,0.));
#16205=DIRECTION('',(-0.052335956242937,-0.998629534754574,0.));
#16206=DIRECTION('',(0.,0.,-1.));
#16207=DIRECTION('',(-1.,0.,0.));
#16208=DIRECTION('',(0.,0.,1.));
#16209=DIRECTION('',(-1.,0.,0.));
#16210=DIRECTION('',(0.,0.,-1.));
#16211=DIRECTION('',(-1.,0.,0.));
#16212=DIRECTION('',(0.,0.,-1.));
#16213=DIRECTION('',(-1.,0.,0.));
#16214=DIRECTION('',(0.,0.,-1.));
#16215=DIRECTION('',(-1.,0.,0.));
#16216=DIRECTION('',(0.,0.,-1.));
#16217=DIRECTION('',(-1.,0.,0.));
#16218=DIRECTION('',(0.,0.,1.));
#16219=DIRECTION('',(1.,0.,0.));
#16220=DIRECTION('',(0.,0.,1.));
#16221=DIRECTION('',(1.,0.,0.));
#16222=DIRECTION('',(0.,0.,-1.));
#16223=DIRECTION('',(-1.,0.,0.));
#16224=DIRECTION('',(0.,0.,-1.));
#16225=DIRECTION('',(-1.,0.,0.));
#16226=DIRECTION('',(0.,0.,-1.));
#16227=DIRECTION('',(-1.,0.,0.));
#16228=DIRECTION('',(0.,0.,-1.));
#16229=DIRECTION('',(-1.,0.,0.));
#16230=DIRECTION('',(0.,0.,-1.));
#16231=DIRECTION('',(-1.,0.,0.));
#16232=DIRECTION('',(0.,0.,-1.));
#16233=DIRECTION('',(-1.,0.,0.));
#16234=DIRECTION('',(0.,0.,-1.));
#16235=DIRECTION('',(-1.,0.,0.));
#16236=DIRECTION('',(0.,0.,-1.));
#16237=DIRECTION('',(-1.,0.,0.));
#16238=DIRECTION('',(0.,0.,-1.));
#16239=DIRECTION('',(-1.,0.,0.));
#16240=DIRECTION('',(0.,0.,-1.));
#16241=DIRECTION('',(-1.,0.,0.));
#16242=DIRECTION('',(0.,0.,1.));
#16243=DIRECTION('',(1.,0.,0.));
#19109=CARTESIAN_POINT('',(0.,0.,0.));
#30741=CARTESIAN_POINT('',(0.00365907271966709,-0.00718133456002582,0.065));
#30742=CARTESIAN_POINT('',(-0.0226621510894003,-0.0205926679525846,0.065));
#30743=CARTESIAN_POINT('',(-0.0222081605896608,-0.0214836744767729,0.065));
#30744=CARTESIAN_POINT('',(-0.0226621510894003,-0.0205926679525846,0.064));
#30745=CARTESIAN_POINT('',(0.00365907271966709,-0.00718133456002582,0.064));
#30746=CARTESIAN_POINT('',(-0.00364987616131558,-0.0109054300239403,0.064));
#30747=CARTESIAN_POINT('',(-0.00356046479940298,-0.0119821988972063,0.065));
#30748=CARTESIAN_POINT('',(-0.00356046479940298,-0.0119821988972063,0.0647249369217302));
#30749=CARTESIAN_POINT('',(-0.00358442462146283,-0.0117264212762759,0.064195847752999));
#30750=CARTESIAN_POINT('',(-0.00362978387837724,-0.0111757204745938,0.064));
#30751=CARTESIAN_POINT('',(-0.00364987616131558,-0.0109054300239404,0.064));
#30752=CARTESIAN_POINT('',(-0.00356046479940298,-0.0119821988972063,0.065));
#30753=CARTESIAN_POINT('',(0.00411306321940664,-0.00807234108421418,0.065));
#30754=CARTESIAN_POINT('',(0.,0.,0.065));
#30755=CARTESIAN_POINT('',(0.00294272257781457,-0.0111171212024526,0.065));
#30756=CARTESIAN_POINT('',(0.00294272257781457,-0.0111171212024526,0.064));
#30757=CARTESIAN_POINT('',(0.00319861149762453,-0.0120838273939702,0.065));
#30758=CARTESIAN_POINT('',(0.,0.,0.065));
#30759=CARTESIAN_POINT('',(0.,0.,0.064));
#30760=CARTESIAN_POINT('',(-0.0217541700899212,-0.0223746810009613,0.065));
#30761=CARTESIAN_POINT('',(-0.0227486623307711,-0.0206394619419116,0.065));
#30762=CARTESIAN_POINT('',(-0.0222514162103461,-0.0215070714714365,0.065));
#30763=CARTESIAN_POINT('',(-0.0227486623307711,-0.0206394619419116,0.064));
#30764=CARTESIAN_POINT('',(-0.0217541700899212,-0.0223746810009613,0.064));
#30765=CARTESIAN_POINT('',(-0.0217541700899212,-0.0223746810009613,0.065));
#30766=CARTESIAN_POINT('',(0.0034545004174345,-0.0130505335854878,0.065));
#30767=CARTESIAN_POINT('',(0.0043624814169136,-0.0112685205371111,0.065));
#30768=CARTESIAN_POINT('',(0.0043624814169136,-0.0112685205371111,0.064));
#30769=CARTESIAN_POINT('',(0.00390849091717405,-0.0121595270612994,0.065));
#30770=CARTESIAN_POINT('',(0.0034545004174345,-0.0130505335854878,0.065));
#30771=CARTESIAN_POINT('',(0.0034545004174345,-0.0130505335854878,0.064));
#30772=CARTESIAN_POINT('',(-0.0217541700899212,-0.0223746810009613,0.064));
#30773=CARTESIAN_POINT('',(-0.0217541700899212,-0.0223746810009613,0.066));
#30774=CARTESIAN_POINT('',(-0.0222081605896608,-0.0214836744767729,0.066));
#30775=CARTESIAN_POINT('',(-0.0222514162103461,-0.0215070714714365,0.066));
#30776=CARTESIAN_POINT('',(-0.0222514162103461,-0.0215070714714365,0.064));
#30777=CARTESIAN_POINT('',(-0.0222081605896608,-0.0214836744767729,0.064));
#30778=CARTESIAN_POINT('',(-0.0036590727196671,-0.00718133456002582,0.065));
#30779=CARTESIAN_POINT('',(0.0226621510894002,-0.0205926679525846,0.065));
#30780=CARTESIAN_POINT('',(0.0226621510894002,-0.0205926679525846,0.064));
#30781=CARTESIAN_POINT('',(0.0222081605896607,-0.0214836744767729,0.065));
#30782=CARTESIAN_POINT('',(0.0222307621135331,-0.0214951905283833,0.065));
#30783=CARTESIAN_POINT('',(0.00401445529914253,-0.011091192373018,0.064));
#30784=CARTESIAN_POINT('',(0.0034545004174345,-0.0130505335854878,0.064));
#30785=CARTESIAN_POINT('',(0.0034545004174345,-0.0130505335854878,0.066));
#30786=CARTESIAN_POINT('',(0.00390849091717405,-0.0121595270612994,0.066));
#30787=CARTESIAN_POINT('',(0.00319861149762453,-0.0120838273939702,0.066));
#30788=CARTESIAN_POINT('',(0.00319861149762453,-0.0120838273939702,0.064));
#30789=CARTESIAN_POINT('',(0.00390849091717405,-0.0121595270612994,0.064));
#30790=CARTESIAN_POINT('',(-0.0217541700899212,-0.0223746810009613,0.066));
#30791=CARTESIAN_POINT('',(-0.0217541700899212,-0.0223746810009613,0.067));
#30792=CARTESIAN_POINT('',(-0.0226621510894003,-0.0205926679525846,0.067));
#30793=CARTESIAN_POINT('',(-0.0227486623307711,-0.0206394619419116,0.067));
#30794=CARTESIAN_POINT('',(-0.0227486623307711,-0.0206394619419116,0.066));
#30795=CARTESIAN_POINT('',(-0.0226621510894003,-0.0205926679525846,0.066));
#30796=CARTESIAN_POINT('',(-0.0302541271933658,-0.00765232343563852,0.065));
#30797=CARTESIAN_POINT('',(-0.0291648491233358,-0.00932966457152937,0.065));
#30798=CARTESIAN_POINT('',(-0.0297094881583508,-0.00849099400358394,0.065));
#30799=CARTESIAN_POINT('',(-0.0291648491233358,-0.00932966457152937,0.064));
#30800=CARTESIAN_POINT('',(-0.0302541271933658,-0.00765232343563852,0.064));
#30801=CARTESIAN_POINT('',(-0.0292486295275229,-0.00938118850960592,0.064));
#30802=CARTESIAN_POINT('',(-0.0292486295275229,-0.00938118850960592,0.065));
#30803=CARTESIAN_POINT('',(-0.0297513783604443,-0.00851675597262222,0.065));
#30804=CARTESIAN_POINT('',(-0.0302541271933658,-0.00765232343563852,0.065));
#30805=CARTESIAN_POINT('',(0.0217541700899211,-0.0223746810009612,0.065));
#30806=CARTESIAN_POINT('',(0.022748662330771,-0.0206394619419116,0.065));
#30807=CARTESIAN_POINT('',(0.022748662330771,-0.0206394619419116,0.064));
#30808=CARTESIAN_POINT('',(0.022251416210346,-0.0215070714714364,0.065));
#30809=CARTESIAN_POINT('',(0.0217541700899211,-0.0223746810009612,0.065));
#30810=CARTESIAN_POINT('',(0.0217541700899211,-0.0223746810009612,0.064));
#30811=CARTESIAN_POINT('',(0.0034545004174345,-0.0130505335854878,0.066));
#30812=CARTESIAN_POINT('',(0.0034545004174345,-0.0130505335854878,0.067));
#30813=CARTESIAN_POINT('',(0.0043624814169136,-0.0112685205371111,0.067));
#30814=CARTESIAN_POINT('',(0.00294272257781457,-0.0111171212024526,0.067));
#30815=CARTESIAN_POINT('',(0.00294272257781457,-0.0111171212024526,0.066));
#30816=CARTESIAN_POINT('',(0.0043624814169136,-0.0112685205371111,0.066));
#30817=CARTESIAN_POINT('',(0.00365907271966709,-0.00718133456002582,0.066));
#30818=CARTESIAN_POINT('',(-0.00356046479940298,-0.0119821988972063,0.066));
#30819=CARTESIAN_POINT('',(-0.00356046479940298,-0.0119821988972063,0.0662750630782698));
#30820=CARTESIAN_POINT('',(-0.00358442462146302,-0.0117264212762759,0.066804152247001));
#30821=CARTESIAN_POINT('',(-0.00362978387837688,-0.0111757204745937,0.067));
#30822=CARTESIAN_POINT('',(-0.00364987616131558,-0.0109054300239404,0.067));
#30823=CARTESIAN_POINT('',(-0.00356046479940298,-0.0119821988972063,0.066));
#30824=CARTESIAN_POINT('',(-0.00364987616131558,-0.0109054300239403,0.067));
#30825=CARTESIAN_POINT('',(-0.00401445529914253,-0.011091192373018,0.067));
#30826=CARTESIAN_POINT('',(-0.0222307621135331,-0.0214951905283833,0.066));
#30827=CARTESIAN_POINT('',(-0.0302541271933658,-0.00765232343563852,0.064));
#30828=CARTESIAN_POINT('',(-0.0302541271933658,-0.00765232343563852,0.066));
#30829=CARTESIAN_POINT('',(-0.0297513783604443,-0.00851675597262222,0.066));
#30830=CARTESIAN_POINT('',(-0.0297094881583508,-0.00849099400358394,0.066));
#30831=CARTESIAN_POINT('',(-0.0297094881583508,-0.00849099400358394,0.067));
#30832=CARTESIAN_POINT('',(-0.0297513783604443,-0.00851675597262222,0.064));
#30833=CARTESIAN_POINT('',(-0.00438968180222396,0.00675951720953923,0.065));
#30834=CARTESIAN_POINT('',(-0.0119400657566617,0.00185624053797081,0.065));
#30835=CARTESIAN_POINT('',(-0.0124847047916767,0.00269491110591624,0.065));
#30836=CARTESIAN_POINT('',(-0.0119400657566617,0.00185624053797081,0.064));
#30837=CARTESIAN_POINT('',(-0.011612482002865,0.00206897591509449,0.064));
#30838=CARTESIAN_POINT('',(-0.0297307621135331,-0.00850480947161671,0.065));
#30839=CARTESIAN_POINT('',(0.0259807621135331,-0.015,0.065));
#30840=CARTESIAN_POINT('',(0.029248629527523,-0.00938118850960603,0.065));
#30841=CARTESIAN_POINT('',(0.029248629527523,-0.00938118850960603,0.064));
#30842=CARTESIAN_POINT('',(0.0297513783604445,-0.00851675597262234,0.065));
#30843=CARTESIAN_POINT('',(0.0259807621135331,-0.015,0.065));
#30844=CARTESIAN_POINT('',(0.0259807621135331,-0.015,0.064));
#30845=CARTESIAN_POINT('',(0.0217541700899211,-0.0223746810009612,0.064));
#30846=CARTESIAN_POINT('',(0.0217541700899211,-0.0223746810009612,0.066));
#30847=CARTESIAN_POINT('',(0.022251416210346,-0.0215070714714364,0.066));
#30848=CARTESIAN_POINT('',(0.0222081605896607,-0.0214836744767729,0.066));
#30849=CARTESIAN_POINT('',(0.0222081605896607,-0.0214836744767729,0.067));
#30850=CARTESIAN_POINT('',(0.022251416210346,-0.0215070714714364,0.064));
#30851=CARTESIAN_POINT('',(-0.0036590727196671,-0.00718133456002582,0.066));
#30852=CARTESIAN_POINT('',(0.0226621510894002,-0.0205926679525846,0.066));
#30853=CARTESIAN_POINT('',(0.0226621510894002,-0.0205926679525846,0.067));
#30854=CARTESIAN_POINT('',(-0.0036590727196671,-0.00718133456002582,0.067));
#30855=CARTESIAN_POINT('',(-0.00411306321940666,-0.00807234108421419,0.066));
#30856=CARTESIAN_POINT('',(0.,0.,0.066));
#30857=CARTESIAN_POINT('',(0.,0.,0.067));
#30858=CARTESIAN_POINT('',(0.,0.,0.066));
#30859=CARTESIAN_POINT('',(-0.0302541271933658,-0.00765232343563852,0.066));
#30860=CARTESIAN_POINT('',(-0.0302541271933658,-0.00765232343563852,0.067));
#30861=CARTESIAN_POINT('',(-0.0292486295275229,-0.00938118850960592,0.067));
#30862=CARTESIAN_POINT('',(-0.0291648491233358,-0.00932966457152937,0.067));
#30863=CARTESIAN_POINT('',(-0.0291648491233358,-0.00932966457152937,0.066));
#30864=CARTESIAN_POINT('',(-0.0292486295275229,-0.00938118850960592,0.066));
#30865=CARTESIAN_POINT('',(-0.0130293438266917,0.00353358167386167,0.065));
#30866=CARTESIAN_POINT('',(-0.0110990706671818,0.00301008809254883,0.065));
#30867=CARTESIAN_POINT('',(-0.0120642072469368,0.00327183488320525,0.065));
#30868=CARTESIAN_POINT('',(-0.0110990706671818,0.00301008809254883,0.064));
#30869=CARTESIAN_POINT('',(-0.0130293438266917,0.00353358167386167,0.064));
#30870=CARTESIAN_POINT('',(-0.0130293438266917,0.00353358167386167,0.065));
#30871=CARTESIAN_POINT('',(0.030254127193366,-0.00765232343563865,0.065));
#30872=CARTESIAN_POINT('',(0.029164849123336,-0.0093296645715295,0.065));
#30873=CARTESIAN_POINT('',(0.029164849123336,-0.0093296645715295,0.064));
#30874=CARTESIAN_POINT('',(0.029709488158351,-0.00849099400358408,0.065));
#30875=CARTESIAN_POINT('',(0.030254127193366,-0.00765232343563865,0.065));
#30876=CARTESIAN_POINT('',(0.030254127193366,-0.00765232343563865,0.064));
#30877=CARTESIAN_POINT('',(0.0217541700899211,-0.0223746810009612,0.066));
#30878=CARTESIAN_POINT('',(0.022748662330771,-0.0206394619419116,0.066));
#30879=CARTESIAN_POINT('',(0.022748662330771,-0.0206394619419116,0.067));
#30880=CARTESIAN_POINT('',(0.0217541700899211,-0.0223746810009612,0.067));
#30881=CARTESIAN_POINT('',(-0.00438968180222396,0.00675951720953923,0.066));
#30882=CARTESIAN_POINT('',(-0.0119400657566617,0.00185624053797081,0.066));
#30883=CARTESIAN_POINT('',(-0.0119400657566617,0.00185624053797081,0.067));
#30884=CARTESIAN_POINT('',(-0.0124847047916767,0.00269491110591624,0.066));
#30885=CARTESIAN_POINT('',(-0.00493432083723898,0.00759818777748466,0.066));
#30886=CARTESIAN_POINT('',(-0.00438968180222396,0.00675951720953923,0.067));
#30887=CARTESIAN_POINT('',(-0.0130293438266917,0.00353358167386167,0.064));
#30888=CARTESIAN_POINT('',(-0.0130293438266917,0.00353358167386167,0.066));
#30889=CARTESIAN_POINT('',(-0.0120642072469368,0.00327183488320525,0.066));
#30890=CARTESIAN_POINT('',(-0.0120642072469368,0.00327183488320525,0.064));
#30891=CARTESIAN_POINT('',(-0.0124847047916767,0.00269491110591624,0.064));
#30892=CARTESIAN_POINT('',(0.,0.,0.065));
#30893=CARTESIAN_POINT('',(-0.00815634808936724,0.00810703310990374,0.065));
#30894=CARTESIAN_POINT('',(-0.00886559574931222,0.00881199251076493,0.065));
#30895=CARTESIAN_POINT('',(-0.00815634808936724,0.00810703310990374,0.064));
#30896=CARTESIAN_POINT('',(0.,0.,0.064));
#30897=CARTESIAN_POINT('',(0.,0.,0.065));
#30898=CARTESIAN_POINT('',(0.00438968180222396,0.00675951720953923,0.065));
#30899=CARTESIAN_POINT('',(0.0119400657566616,0.00185624053797081,0.065));
#30900=CARTESIAN_POINT('',(0.0119400657566616,0.00185624053797081,0.064));
#30901=CARTESIAN_POINT('',(0.0124847047916767,0.00269491110591624,0.065));
#30902=CARTESIAN_POINT('',(0.00493432083723899,0.00759818777748466,0.065));
#30903=CARTESIAN_POINT('',(0.00438968180222396,0.00675951720953923,0.064));
#30904=CARTESIAN_POINT('',(0.030254127193366,-0.00765232343563865,0.064));
#30905=CARTESIAN_POINT('',(0.030254127193366,-0.00765232343563865,0.066));
#30906=CARTESIAN_POINT('',(0.029709488158351,-0.00849099400358408,0.066));
#30907=CARTESIAN_POINT('',(0.0297513783604445,-0.00851675597262234,0.066));
#30908=CARTESIAN_POINT('',(0.0297513783604445,-0.00851675597262234,0.064));
#30909=CARTESIAN_POINT('',(0.029709488158351,-0.00849099400358408,0.064));
#30910=CARTESIAN_POINT('',(0.0259807621135331,-0.015,0.066));
#30911=CARTESIAN_POINT('',(0.029248629527523,-0.00938118850960603,0.066));
#30912=CARTESIAN_POINT('',(0.029248629527523,-0.00938118850960603,0.067));
#30913=CARTESIAN_POINT('',(0.0259807621135331,-0.015,0.067));
#30914=CARTESIAN_POINT('',(0.0259807621135331,-0.015,0.066));
#30915=CARTESIAN_POINT('',(-0.0130293438266917,0.00353358167386167,0.066));
#30916=CARTESIAN_POINT('',(-0.0130293438266917,0.00353358167386167,0.067));
#30917=CARTESIAN_POINT('',(-0.0110990706671818,0.00301008809254883,0.067));
#30918=CARTESIAN_POINT('',(-0.0110990706671818,0.00301008809254883,0.066));
#30919=CARTESIAN_POINT('',(-0.0095748434092572,0.00951695191162613,0.065));
#30920=CARTESIAN_POINT('',(-0.00757758433974805,0.00941227999914025,0.065));
#30921=CARTESIAN_POINT('',(-0.00857621387450262,0.00946461595538319,0.065));
#30922=CARTESIAN_POINT('',(-0.00757758433974805,0.00941227999914025,0.064));
#30923=CARTESIAN_POINT('',(-0.0095748434092572,0.00951695191162613,0.064));
#30924=CARTESIAN_POINT('',(-0.0095748434092572,0.00951695191162613,0.065));
#30925=CARTESIAN_POINT('',(0.0130293438266917,0.00353358167386167,0.065));
#30926=CARTESIAN_POINT('',(0.0110990706671818,0.00301008809254883,0.065));
#30927=CARTESIAN_POINT('',(0.0110990706671818,0.00301008809254883,0.064));
#30928=CARTESIAN_POINT('',(0.0120642072469368,0.00327183488320525,0.065));
#30929=CARTESIAN_POINT('',(0.0130293438266917,0.00353358167386167,0.065));
#30930=CARTESIAN_POINT('',(0.0130293438266917,0.00353358167386167,0.064));
#30931=CARTESIAN_POINT('',(0.030254127193366,-0.00765232343563865,0.066));
#30932=CARTESIAN_POINT('',(0.029164849123336,-0.0093296645715295,0.066));
#30933=CARTESIAN_POINT('',(0.029164849123336,-0.0093296645715295,0.067));
#30934=CARTESIAN_POINT('',(0.030254127193366,-0.00765232343563865,0.067));
#30935=CARTESIAN_POINT('',(0.,0.,0.066));
#30936=CARTESIAN_POINT('',(-0.00815634808936724,0.00810703310990374,0.066));
#30937=CARTESIAN_POINT('',(-0.00815634808936724,0.00810703310990374,0.067));
#30938=CARTESIAN_POINT('',(-0.00886559574931222,0.00881199251076493,0.066));
#30939=CARTESIAN_POINT('',(0.,0.,0.066));
#30940=CARTESIAN_POINT('',(0.,0.,0.067));
#30941=CARTESIAN_POINT('',(-0.0095748434092572,0.00951695191162613,0.064));
#30942=CARTESIAN_POINT('',(-0.0095748434092572,0.00951695191162613,0.066));
#30943=CARTESIAN_POINT('',(-0.00857621387450262,0.00946461595538319,0.066));
#30944=CARTESIAN_POINT('',(-0.00857621387450262,0.00946461595538319,0.064));
#30945=CARTESIAN_POINT('',(-0.00886559574931222,0.00881199251076493,0.064));
#30946=CARTESIAN_POINT('',(-0.00804875452189106,0.000421817350486591,0.065));
#30947=CARTESIAN_POINT('',(-0.00650269803393578,0.029922332524114,0.065));
#30948=CARTESIAN_POINT('',(-0.00750132756869036,0.029974668480357,0.065));
#30949=CARTESIAN_POINT('',(-0.00650269803393578,0.029922332524114,0.064));
#30950=CARTESIAN_POINT('',(-0.00804875452189106,0.000421817350486591,0.064));
#30951=CARTESIAN_POINT('',(-0.00904738405664563,0.000474153306729528,0.065));
#30952=CARTESIAN_POINT('',(0.,0.,0.065));
#30953=CARTESIAN_POINT('',(0.00815634808936724,0.00810703310990373,0.065));
#30954=CARTESIAN_POINT('',(0.00815634808936724,0.00810703310990373,0.064));
#30955=CARTESIAN_POINT('',(0.00886559574931222,0.00881199251076493,0.065));
#30956=CARTESIAN_POINT('',(0.,0.,0.065));
#30957=CARTESIAN_POINT('',(0.,0.,0.064));
#30958=CARTESIAN_POINT('',(0.0130293438266917,0.00353358167386167,0.064));
#30959=CARTESIAN_POINT('',(0.0130293438266917,0.00353358167386167,0.066));
#30960=CARTESIAN_POINT('',(0.0120642072469368,0.00327183488320525,0.066));
#30961=CARTESIAN_POINT('',(0.0124847047916767,0.00269491110591624,0.066));
#30962=CARTESIAN_POINT('',(0.0124847047916767,0.00269491110591624,0.064));
#30963=CARTESIAN_POINT('',(0.0120642072469368,0.00327183488320525,0.064));
#30964=CARTESIAN_POINT('',(0.00438968180222396,0.00675951720953923,0.066));
#30965=CARTESIAN_POINT('',(0.0119400657566616,0.00185624053797081,0.066));
#30966=CARTESIAN_POINT('',(0.0119400657566616,0.00185624053797081,0.067));
#30967=CARTESIAN_POINT('',(0.011612482002865,0.00206897591509449,0.067));
#30968=CARTESIAN_POINT('',(0.0297307621135331,-0.00850480947161673,0.066));
#30969=CARTESIAN_POINT('',(-0.0095748434092572,0.00951695191162613,0.066));
#30970=CARTESIAN_POINT('',(-0.0095748434092572,0.00951695191162613,0.067));
#30971=CARTESIAN_POINT('',(-0.00757758433974805,0.00941227999914025,0.067));
#30972=CARTESIAN_POINT('',(-0.00757758433974805,0.00941227999914025,0.066));
#30973=CARTESIAN_POINT('',(-0.00849995710344493,0.0300270044365999,0.065));
#30974=CARTESIAN_POINT('',(-0.00649996719675201,0.0300206504515176,0.065));
#30975=CARTESIAN_POINT('',(-0.00749996215009847,0.0300238274440587,0.065));
#30976=CARTESIAN_POINT('',(-0.00649996719675201,0.0300206504515176,0.064));
#30977=CARTESIAN_POINT('',(-0.00849995710344493,0.0300270044365999,0.064));
#30978=CARTESIAN_POINT('',(-0.00849995710344493,0.0300270044365999,0.065));
#30979=CARTESIAN_POINT('',(0.0095748434092572,0.00951695191162612,0.065));
#30980=CARTESIAN_POINT('',(0.00757758433974805,0.00941227999914025,0.065));
#30981=CARTESIAN_POINT('',(0.00757758433974805,0.00941227999914025,0.064));
#30982=CARTESIAN_POINT('',(0.00857621387450262,0.00946461595538318,0.065));
#30983=CARTESIAN_POINT('',(0.0095748434092572,0.00951695191162612,0.065));
#30984=CARTESIAN_POINT('',(0.0095748434092572,0.00951695191162612,0.064));
#30985=CARTESIAN_POINT('',(0.0130293438266917,0.00353358167386167,0.066));
#30986=CARTESIAN_POINT('',(0.0110990706671818,0.00301008809254883,0.066));
#30987=CARTESIAN_POINT('',(0.0110990706671818,0.00301008809254883,0.067));
#30988=CARTESIAN_POINT('',(0.0130293438266917,0.00353358167386167,0.067));
#30989=CARTESIAN_POINT('',(-0.00804875452189106,0.000421817350486591,0.066));
#30990=CARTESIAN_POINT('',(-0.00650269803393578,0.029922332524114,0.066));
#30991=CARTESIAN_POINT('',(-0.00650269803393578,0.029922332524114,0.067));
#30992=CARTESIAN_POINT('',(-0.00750132756869036,0.029974668480357,0.066));
#30993=CARTESIAN_POINT('',(-0.0075,0.03,0.066));
#30994=CARTESIAN_POINT('',(-0.0075980267037225,0.00902221645792347,0.067));
#30995=CARTESIAN_POINT('',(-0.00849995710344493,0.0300270044365999,0.064));
#30996=CARTESIAN_POINT('',(-0.00849995710344493,0.0300270044365999,0.066));
#30997=CARTESIAN_POINT('',(-0.00749996215009847,0.0300238274440587,0.066));
#30998=CARTESIAN_POINT('',(-0.00749996215009847,0.0300238274440587,0.064));
#30999=CARTESIAN_POINT('',(-0.00750132756869036,0.029974668480357,0.064));
#31000=CARTESIAN_POINT('',(0.,0.03,0.065));
#31001=CARTESIAN_POINT('',(0.00649996719675201,0.0300206504515176,0.065));
#31002=CARTESIAN_POINT('',(0.00749996215009847,0.0300238274440587,0.065));
#31003=CARTESIAN_POINT('',(0.00649996719675201,0.0300206504515176,0.064));
#31004=CARTESIAN_POINT('',(0.,0.03,0.064));
#31005=CARTESIAN_POINT('',(0.,0.03,0.065));
#31006=CARTESIAN_POINT('',(0.00804875452189106,0.000421817350486591,0.065));
#31007=CARTESIAN_POINT('',(0.00650269803393578,0.029922332524114,0.065));
#31008=CARTESIAN_POINT('',(0.00650269803393578,0.029922332524114,0.064));
#31009=CARTESIAN_POINT('',(0.00750132756869036,0.029974668480357,0.065));
#31010=CARTESIAN_POINT('',(0.0075,0.03,0.065));
#31011=CARTESIAN_POINT('',(0.0075980267037225,0.00902221645792347,0.064));
#31012=CARTESIAN_POINT('',(0.0095748434092572,0.00951695191162612,0.064));
#31013=CARTESIAN_POINT('',(0.0095748434092572,0.00951695191162612,0.066));
#31014=CARTESIAN_POINT('',(0.00857621387450262,0.00946461595538318,0.066));
#31015=CARTESIAN_POINT('',(0.00886559574931222,0.00881199251076493,0.066));
#31016=CARTESIAN_POINT('',(0.00886559574931222,0.00881199251076493,0.064));
#31017=CARTESIAN_POINT('',(0.00857621387450262,0.00946461595538318,0.064));
#31018=CARTESIAN_POINT('',(0.,0.,0.066));
#31019=CARTESIAN_POINT('',(0.00815634808936724,0.00810703310990373,0.066));
#31020=CARTESIAN_POINT('',(0.00815634808936724,0.00810703310990373,0.067));
#31021=CARTESIAN_POINT('',(0.,0.,0.067));
#31022=CARTESIAN_POINT('',(0.,0.,0.066));
#31023=CARTESIAN_POINT('',(-0.00849995710344493,0.0300270044365999,0.066));
#31024=CARTESIAN_POINT('',(-0.00849995710344493,0.0300270044365999,0.067));
#31025=CARTESIAN_POINT('',(-0.00649996719675201,0.0300206504515176,0.067));
#31026=CARTESIAN_POINT('',(-0.00649996719675201,0.0300206504515176,0.066));
#31027=CARTESIAN_POINT('',(0.00849995710344493,0.0300270044365999,0.065));
#31028=CARTESIAN_POINT('',(0.00849995710344493,0.0300270044365999,0.065));
#31029=CARTESIAN_POINT('',(0.00849995710344493,0.0300270044365999,0.064));
#31030=CARTESIAN_POINT('',(0.0095748434092572,0.00951695191162612,0.066));
#31031=CARTESIAN_POINT('',(0.00757758433974805,0.00941227999914025,0.066));
#31032=CARTESIAN_POINT('',(0.00757758433974805,0.00941227999914025,0.067));
#31033=CARTESIAN_POINT('',(0.0095748434092572,0.00951695191162612,0.067));
#31034=CARTESIAN_POINT('',(0.,0.03,0.066));
#31035=CARTESIAN_POINT('',(0.00649996719675201,0.0300206504515176,0.066));
#31036=CARTESIAN_POINT('',(0.00649996719675201,0.0300206504515176,0.067));
#31037=CARTESIAN_POINT('',(0.00749996215009847,0.0300238274440587,0.066));
#31038=CARTESIAN_POINT('',(0.,0.03,0.066));
#31039=CARTESIAN_POINT('',(0.,0.03,0.067));
#31040=CARTESIAN_POINT('',(0.00849995710344493,0.0300270044365999,0.064));
#31041=CARTESIAN_POINT('',(0.00849995710344493,0.0300270044365999,0.066));
#31042=CARTESIAN_POINT('',(0.00750132756869036,0.029974668480357,0.066));
#31043=CARTESIAN_POINT('',(0.00750132756869036,0.029974668480357,0.067));
#31044=CARTESIAN_POINT('',(0.00749996215009847,0.0300238274440587,0.064));
#31045=CARTESIAN_POINT('',(0.00804875452189106,0.000421817350486591,0.066));
#31046=CARTESIAN_POINT('',(0.00650269803393578,0.029922332524114,0.066));
#31047=CARTESIAN_POINT('',(0.00650269803393578,0.029922332524114,0.067));
#31048=CARTESIAN_POINT('',(0.00804875452189106,0.000421817350486591,0.067));
#31049=CARTESIAN_POINT('',(0.00904738405664563,0.000474153306729528,0.066));
#31050=CARTESIAN_POINT('',(0.00849995710344493,0.0300270044365999,0.066));
#31051=CARTESIAN_POINT('',(0.00849995710344493,0.0300270044365999,0.067));
#31052=CARTESIAN_POINT('',(-0.024761562113538,-0.0149999999999972,0.066269998));
#31053=CARTESIAN_POINT('',(0.,0.03,0.066269998));
#31054=CARTESIAN_POINT('',(-0.00277876,0.03,0.066269998));
#31055=CARTESIAN_POINT('',(0.,0.03,0.066269998));
#31056=CARTESIAN_POINT('',(-0.0012192,0.03,0.066269998));
#31057=CARTESIAN_POINT('',(-0.024761562113538,-0.0149999999999972,0.066269998));
#31058=CARTESIAN_POINT('',(0.0259807621135283,-0.0150000000000028,0.066269998));
#31059=CARTESIAN_POINT('',(0.0232020021135283,-0.0150000000000028,0.066269998));
#31060=CARTESIAN_POINT('',(0.0259807621135283,-0.0150000000000028,0.066269998));
#31061=CARTESIAN_POINT('',(0.0247615621135283,-0.0150000000000028,0.066269998));
#31062=CARTESIAN_POINT('',(-0.024761562113538,-0.0149999999999972,0.066269998));
#31063=CARTESIAN_POINT('',(-0.025980762113538,-0.0149999999999972,0.066269998));
#31064=CARTESIAN_POINT('',(-0.028759522113538,-0.0149999999999972,0.066269998));
#31065=CARTESIAN_POINT('',(-0.025980762113538,-0.0149999999999972,0.066269998));
#31066=CARTESIAN_POINT('',(-0.027199962113538,-0.0149999999999972,0.066269998));
#31067=CARTESIAN_POINT('',(-0.00753201094464286,0.,0.0662062500024776));
#31068=CARTESIAN_POINT('',(-0.00753201094464286,0.00244729870815628,0.0661155357167633));
#31069=CARTESIAN_POINT('',(-0.00609352485603417,0.00442720495336657,0.066024821431049));
#31070=CARTESIAN_POINT('',(-0.00465503876742549,0.00640711119857685,0.0659341071453347));
#31071=CARTESIAN_POINT('',(-0.00232751938371274,0.00716336808970901,0.0658433928596205));
#31072=CARTESIAN_POINT('',(-4.84937169161726E-19,0.00791962498084115,0.0657526785739062));
#31073=CARTESIAN_POINT('',(0.00232751938371274,0.00716336808970901,0.0656619642881919));
#31074=CARTESIAN_POINT('',(0.00465503876742549,0.00640711119857685,0.0655712500024775));
#31075=CARTESIAN_POINT('',(0.00609352485603417,0.00442720495336657,0.0654805357167633));
#31076=CARTESIAN_POINT('',(0.00753201094464286,0.00244729870815628,0.065389821431049));
#31077=CARTESIAN_POINT('',(0.00753201094464286,9.22405309449971E-19,0.0652991071453347));
#31078=CARTESIAN_POINT('',(0.00753201094464286,-0.00244729870815628,0.0652083928596204));
#31079=CARTESIAN_POINT('',(0.00609352485603417,-0.00442720495336657,0.0651176785739062));
#31080=CARTESIAN_POINT('',(0.00465503876742549,-0.00640711119857685,0.0650269642881918));
#31081=CARTESIAN_POINT('',(0.00232751938371274,-0.00716336808970901,0.0649362500024776));
#31082=CARTESIAN_POINT('',(1.45481150748518E-18,-0.00791962498084115,0.0648455357167633));
#31083=CARTESIAN_POINT('',(-0.00232751938371274,-0.00716336808970901,0.064754821431049));
#31084=CARTESIAN_POINT('',(-0.00465503876742549,-0.00640711119857685,0.0646641071453347));
#31085=CARTESIAN_POINT('',(-0.00609352485603417,-0.00442720495336658,0.0645733928596205));
#31086=CARTESIAN_POINT('',(-0.00753201094464286,-0.00244729870815628,0.0644826785739061));
#31087=CARTESIAN_POINT('',(-0.00753201094464286,0.,0.0643919642881919));
#31088=CARTESIAN_POINT('',(-0.00753201094464286,0.00244729870815628,0.0643012500024776));
#31089=CARTESIAN_POINT('',(-0.00609352485603417,0.00442720495336657,0.0642105357167633));
#31090=CARTESIAN_POINT('',(-0.00465503876742549,0.00640711119857685,0.064119821431049));
#31091=CARTESIAN_POINT('',(-0.00232751938371274,0.00716336808970901,0.0640291071453348));
#31092=CARTESIAN_POINT('',(-4.84937169161726E-19,0.00791962498084115,0.0639383928596205));
#31093=CARTESIAN_POINT('',(0.00232751938371274,0.00716336808970901,0.0638476785739062));
#31094=CARTESIAN_POINT('',(0.00465503876742549,0.00640711119857685,0.0637569642881919));
#31095=CARTESIAN_POINT('',(0.00609352485603417,0.00442720495336657,0.0636662500024776));
#31096=CARTESIAN_POINT('',(0.00753201094464286,0.00244729870815628,0.0635755357167633));
#31097=CARTESIAN_POINT('',(0.00753201094464286,9.22405309449971E-19,0.063484821431049));
#31098=CARTESIAN_POINT('',(0.00753201094464286,-0.00244729870815628,0.0633941071453348));
#31099=CARTESIAN_POINT('',(0.00609352485603417,-0.00442720495336657,0.0633033928596205));
#31100=CARTESIAN_POINT('',(0.00534171614397317,-0.00546198087230006,0.0632559820498473));
#31101=CARTESIAN_POINT('',(0.0042904607332246,-0.00619056827495487,0.0632061437275364));
#31102=CARTESIAN_POINT('',(-0.00655,0.,0.0656392857192409));
#31103=CARTESIAN_POINT('',(-0.00655,0.00212822401032553,0.0655485714335265));
#31104=CARTESIAN_POINT('',(-0.00529906131315591,0.0038499934025157,0.0654578571478123));
#31105=CARTESIAN_POINT('',(-0.00404812262631181,0.00557176279470586,0.065367142862098));
#31106=CARTESIAN_POINT('',(-0.0020240613131559,0.00622942018173326,0.0652764285763837));
#31107=CARTESIAN_POINT('',(-4.21711875003113E-19,0.00688707756876065,0.0651857142906694));
#31108=CARTESIAN_POINT('',(0.0020240613131559,0.00622942018173326,0.0650950000049552));
#31109=CARTESIAN_POINT('',(0.00404812262631181,0.00557176279470586,0.0650042857192408));
#31110=CARTESIAN_POINT('',(0.00529906131315591,0.0038499934025157,0.0649135714335266));
#31111=CARTESIAN_POINT('',(0.00655,0.00212822401032553,0.0648228571478123));
#31112=CARTESIAN_POINT('',(0.00655,8.02143653441516E-19,0.064732142862098));
#31113=CARTESIAN_POINT('',(0.00655,-0.00212822401032553,0.0646414285763837));
#31114=CARTESIAN_POINT('',(0.00529906131315591,-0.0038499934025157,0.0645507142906695));
#31115=CARTESIAN_POINT('',(0.00404812262631181,-0.00557176279470586,0.0644600000049551));
#31116=CARTESIAN_POINT('',(0.0020240613131559,-0.00622942018173326,0.0643692857192409));
#31117=CARTESIAN_POINT('',(1.26513562500934E-18,-0.00688707756876065,0.0642785714335266));
#31118=CARTESIAN_POINT('',(-0.0020240613131559,-0.00622942018173326,0.0641878571478123));
#31119=CARTESIAN_POINT('',(-0.00404812262631181,-0.00557176279470586,0.064097142862098));
#31120=CARTESIAN_POINT('',(-0.00529906131315591,-0.0038499934025157,0.0640064285763837));
#31121=CARTESIAN_POINT('',(-0.00655,-0.00212822401032553,0.0639157142906694));
#31122=CARTESIAN_POINT('',(-0.00655,0.,0.0638250000049552));
#31123=CARTESIAN_POINT('',(-0.00655,0.00212822401032553,0.0637342857192409));
#31124=CARTESIAN_POINT('',(-0.00529906131315591,0.0038499934025157,0.0636435714335266));
#31125=CARTESIAN_POINT('',(-0.00404812262631181,0.00557176279470586,0.0635528571478123));
#31126=CARTESIAN_POINT('',(-0.0020240613131559,0.00622942018173326,0.063462142862098));
#31127=CARTESIAN_POINT('',(-4.21711875003113E-19,0.00688707756876065,0.0633714285763838));
#31128=CARTESIAN_POINT('',(0.0020240613131559,0.00622942018173326,0.0632807142906695));
#31129=CARTESIAN_POINT('',(0.00404812262631181,0.00557176279470586,0.0631900000049551));
#31130=CARTESIAN_POINT('',(0.00529906131315591,0.0038499934025157,0.0630992857192409));
#31131=CARTESIAN_POINT('',(0.00655,0.00212822401032553,0.0630085714335265));
#31132=CARTESIAN_POINT('',(0.00655,8.02143653441516E-19,0.0629178571478123));
#31133=CARTESIAN_POINT('',(0.00655,-0.00212822401032553,0.062827142862098));
#31134=CARTESIAN_POINT('',(0.00529906131315591,-0.0038499934025157,0.0627364285763837));
#31135=CARTESIAN_POINT('',(0.00464527215907854,-0.00474985697398794,0.0626890177666106));
#31136=CARTESIAN_POINT('',(0.00373107766427357,-0.00538345237400303,0.0626391794442997));
#31137=CARTESIAN_POINT('',(-0.00704100547232143,0.,0.0659227678608592));
#31138=CARTESIAN_POINT('',(-0.00753201094464286,0.,0.0662062500024776));
#31139=CARTESIAN_POINT('',(-0.00655,0.,0.0656392857192409));
#31140=CARTESIAN_POINT('',(-0.00655,0.,0.0656392857192409));
#31141=CARTESIAN_POINT('',(-0.00655,0.00212822401032553,0.0655485714335265));
#31142=CARTESIAN_POINT('',(-0.00529906131315591,0.0038499934025157,0.0654578571478123));
#31143=CARTESIAN_POINT('',(-0.00404812262631181,0.00557176279470586,0.065367142862098));
#31144=CARTESIAN_POINT('',(-0.0020240613131559,0.00622942018173326,0.0652764285763837));
#31145=CARTESIAN_POINT('',(-4.21711875003113E-19,0.00688707756876065,0.0651857142906694));
#31146=CARTESIAN_POINT('',(0.0020240613131559,0.00622942018173326,0.0650950000049552));
#31147=CARTESIAN_POINT('',(0.00404812262631181,0.00557176279470586,0.0650042857192408));
#31148=CARTESIAN_POINT('',(0.00529906131315591,0.0038499934025157,0.0649135714335266));
#31149=CARTESIAN_POINT('',(0.00654999999999999,0.00212822401032555,0.0648228571478123));
#31150=CARTESIAN_POINT('',(0.00655,8.02143653441516E-19,0.064732142862098));
#31151=CARTESIAN_POINT('',(0.00655,8.02143653441516E-19,0.064732142862098));
#31152=CARTESIAN_POINT('',(0.00655,8.02143653441517E-19,0.064732142862098));
#31153=CARTESIAN_POINT('',(0.00655000000000001,-0.00212822401032553,0.0646414285763838));
#31154=CARTESIAN_POINT('',(0.00529906131315591,-0.0038499934025157,0.0645507142906695));
#31155=CARTESIAN_POINT('',(0.00404812262631181,-0.00557176279470586,0.0644600000049551));
#31156=CARTESIAN_POINT('',(0.0020240613131559,-0.00622942018173326,0.0643692857192409));
#31157=CARTESIAN_POINT('',(1.26513562500934E-18,-0.00688707756876065,0.0642785714335266));
#31158=CARTESIAN_POINT('',(-0.0020240613131559,-0.00622942018173326,0.0641878571478123));
#31159=CARTESIAN_POINT('',(-0.00404812262631181,-0.00557176279470586,0.064097142862098));
#31160=CARTESIAN_POINT('',(-0.00529906131315591,-0.0038499934025157,0.0640064285763837));
#31161=CARTESIAN_POINT('',(-0.00654999999999999,-0.00212822401032555,0.0639157142906695));
#31162=CARTESIAN_POINT('',(-0.00655,0.,0.0638250000049552));
#31163=CARTESIAN_POINT('',(-0.00655,0.,0.0638250000049552));
#31164=CARTESIAN_POINT('',(-0.00655,0.,0.0638250000049552));
#31165=CARTESIAN_POINT('',(-0.00655000000000001,0.00212822401032553,0.0637342857192409));
#31166=CARTESIAN_POINT('',(-0.00529906131315591,0.0038499934025157,0.0636435714335266));
#31167=CARTESIAN_POINT('',(-0.00404812262631181,0.00557176279470586,0.0635528571478123));
#31168=CARTESIAN_POINT('',(-0.0020240613131559,0.00622942018173326,0.063462142862098));
#31169=CARTESIAN_POINT('',(-4.21711875003113E-19,0.00688707756876065,0.0633714285763838));
#31170=CARTESIAN_POINT('',(0.0020240613131559,0.00622942018173326,0.0632807142906695));
#31171=CARTESIAN_POINT('',(0.00404812262631181,0.00557176279470586,0.0631900000049551));
#31172=CARTESIAN_POINT('',(0.00529906131315591,0.0038499934025157,0.0630992857192409));
#31173=CARTESIAN_POINT('',(0.00654999999999999,0.00212822401032556,0.0630085714335266));
#31174=CARTESIAN_POINT('',(0.00655,8.02143653441516E-19,0.0629178571478123));
#31175=CARTESIAN_POINT('',(0.00655,8.02143653441516E-19,0.0629178571478123));
#31176=CARTESIAN_POINT('',(0.00655,8.02143653441517E-19,0.0629178571478123));
#31177=CARTESIAN_POINT('',(0.00655000000000002,-0.00212822401032552,0.062827142862098));
#31178=CARTESIAN_POINT('',(0.00529906131315591,-0.0038499934025157,0.0627364285763837));
#31179=CARTESIAN_POINT('',(0.00464527215907854,-0.00474985697398794,0.0626890177666106));
#31180=CARTESIAN_POINT('',(0.00373107766427357,-0.00538345237400303,0.0626391794442997));
#31181=CARTESIAN_POINT('',(0.00373107766427358,-0.00538345237400303,0.0626391794442997));
#31182=CARTESIAN_POINT('',(0.00401076919874908,-0.00578701032447895,0.0629226615859181));
#31183=CARTESIAN_POINT('',(0.0042904607332246,-0.00619056827495487,0.0632061437275364));
#31184=CARTESIAN_POINT('',(-0.00753201094464286,0.,0.0662062500024776));
#31185=CARTESIAN_POINT('',(-0.00753201094464286,0.00244729870815628,0.0661155357167633));
#31186=CARTESIAN_POINT('',(-0.00609352485603417,0.00442720495336657,0.066024821431049));
#31187=CARTESIAN_POINT('',(-0.00465503876742549,0.00640711119857685,0.0659341071453347));
#31188=CARTESIAN_POINT('',(-0.00232751938371274,0.00716336808970901,0.0658433928596205));
#31189=CARTESIAN_POINT('',(-4.84937169161726E-19,0.00791962498084115,0.0657526785739062));
#31190=CARTESIAN_POINT('',(0.00232751938371274,0.00716336808970901,0.0656619642881919));
#31191=CARTESIAN_POINT('',(0.00465503876742549,0.00640711119857685,0.0655712500024775));
#31192=CARTESIAN_POINT('',(0.00609352485603417,0.00442720495336657,0.0654805357167633));
#31193=CARTESIAN_POINT('',(0.00753201094464286,0.00244729870815628,0.065389821431049));
#31194=CARTESIAN_POINT('',(0.00753201094464286,9.22405309449971E-19,0.0652991071453347));
#31195=CARTESIAN_POINT('',(0.00753201094464286,-0.00244729870815628,0.0652083928596204));
#31196=CARTESIAN_POINT('',(0.00609352485603417,-0.00442720495336657,0.0651176785739062));
#31197=CARTESIAN_POINT('',(0.00465503876742549,-0.00640711119857685,0.0650269642881918));
#31198=CARTESIAN_POINT('',(0.00232751938371274,-0.00716336808970901,0.0649362500024776));
#31199=CARTESIAN_POINT('',(1.45481150748518E-18,-0.00791962498084115,0.0648455357167633));
#31200=CARTESIAN_POINT('',(-0.00232751938371274,-0.00716336808970901,0.064754821431049));
#31201=CARTESIAN_POINT('',(-0.00465503876742549,-0.00640711119857685,0.0646641071453347));
#31202=CARTESIAN_POINT('',(-0.00609352485603417,-0.00442720495336658,0.0645733928596205));
#31203=CARTESIAN_POINT('',(-0.00753201094464286,-0.00244729870815628,0.0644826785739061));
#31204=CARTESIAN_POINT('',(-0.00753201094464286,0.,0.0643919642881919));
#31205=CARTESIAN_POINT('',(-0.00753201094464286,0.00244729870815628,0.0643012500024776));
#31206=CARTESIAN_POINT('',(-0.00609352485603417,0.00442720495336657,0.0642105357167633));
#31207=CARTESIAN_POINT('',(-0.00465503876742549,0.00640711119857685,0.064119821431049));
#31208=CARTESIAN_POINT('',(-0.00232751938371274,0.00716336808970901,0.0640291071453348));
#31209=CARTESIAN_POINT('',(-4.84937169161726E-19,0.00791962498084115,0.0639383928596205));
#31210=CARTESIAN_POINT('',(0.00232751938371274,0.00716336808970901,0.0638476785739062));
#31211=CARTESIAN_POINT('',(0.00465503876742549,0.00640711119857685,0.0637569642881919));
#31212=CARTESIAN_POINT('',(0.00609352485603417,0.00442720495336657,0.0636662500024776));
#31213=CARTESIAN_POINT('',(0.00753201094464286,0.00244729870815628,0.0635755357167633));
#31214=CARTESIAN_POINT('',(0.00753201094464286,9.22405309449971E-19,0.063484821431049));
#31215=CARTESIAN_POINT('',(0.00753201094464286,-0.00244729870815628,0.0633941071453348));
#31216=CARTESIAN_POINT('',(0.00609352485603417,-0.00442720495336657,0.0633033928596205));
#31217=CARTESIAN_POINT('',(0.00534171614397317,-0.00546198087230006,0.0632559820498473));
#31218=CARTESIAN_POINT('',(0.0042904607332246,-0.00619056827495487,0.0632061437275364));
#31219=CARTESIAN_POINT('',(-0.00655,0.,0.067));
#31220=CARTESIAN_POINT('',(-0.00655,0.000701436451549039,0.0669701016874316));
#31221=CARTESIAN_POINT('',(-0.00643426444377327,0.00142116428632275,0.0669378208348473));
#31222=CARTESIAN_POINT('',(-0.00597275524955853,0.00278310287089703,0.0668733773348871));
#31223=CARTESIAN_POINT('',(-0.00563065184170616,0.00341964341195903,0.0668419312518172));
#31224=CARTESIAN_POINT('',(-0.00477526447734829,0.00453817699069122,0.0667814502995436));
#31225=CARTESIAN_POINT('',(-0.00424468348110516,0.00504002014029157,0.0667489920151821));
#31226=CARTESIAN_POINT('',(-0.00305067784563627,0.00584059119879621,0.0666846094693261));
#31227=CARTESIAN_POINT('',(-0.00239715639327556,0.00613638840539808,0.0666538642150764));
#31228=CARTESIAN_POINT('',(-0.00103349869292125,0.00650642005156875,0.0665927478677392));
#31229=CARTESIAN_POINT('',(-0.000306008953235865,0.00658216137226912,0.0665601432664502));
#31230=CARTESIAN_POINT('',(0.00112780996837254,0.00649203623567304,0.0664958824367649));
#31231=CARTESIAN_POINT('',(0.00182250228407492,0.00633113339858685,0.0664657019759955));
#31232=CARTESIAN_POINT('',(0.00313452003775661,0.00579478634800822,0.0664040010301873));
#31233=CARTESIAN_POINT('',(0.00375876413031788,0.00541195045606427,0.0663712817114677));
#31234=CARTESIAN_POINT('',(0.00484143708566559,0.00446967587994929,0.0663072029772139));
#31235=CARTESIAN_POINT('',(0.00529358804533871,0.00392244160944412,0.0662774495781941));
#31236=CARTESIAN_POINT('',(0.00601170596849487,0.00269573995808473,0.0662152165673029));
#31237=CARTESIAN_POINT('',(0.00627453396340782,0.00201157756744779,0.06618241451258));
#31238=CARTESIAN_POINT('',(0.00656107801575611,0.000607022272226752,0.0661185776819682));
#31239=CARTESIAN_POINT('',(0.0065878793671143,-0.000100163932046034,0.0660891123253293));
#31240=CARTESIAN_POINT('',(0.00641225008508753,-0.00151434349314421,0.0660264013812344));
#31241=CARTESIAN_POINT('',(0.00620457950132945,-0.00221761186551469,0.0659935488484532));
#31242=CARTESIAN_POINT('',(0.00557935079068769,-0.00350506118760313,0.0659300129741499));
#31243=CARTESIAN_POINT('',(0.00517180671586844,-0.00408226252975466,0.0659006957696452));
#31244=CARTESIAN_POINT('',(0.00417062794027762,-0.00510081509681702,0.065837562474521));
#31245=CARTESIAN_POINT('',(0.00357788920975624,-0.0055327564608861,0.0658046918907707));
#31246=CARTESIAN_POINT('',(0.00230128976425064,-0.00617387647055902,0.0657415150903395));
#31247=CARTESIAN_POINT('',(0.00162702620582906,-0.00638491943224267,0.0657122056990415));
#31248=CARTESIAN_POINT('',(0.000210210709061308,-0.00658560717690332,0.0656487069280592));
#31249=CARTESIAN_POINT('',(-0.000522891642424388,-0.00656787931369974,0.0656158507809958));
#31250=CARTESIAN_POINT('',(-0.00192323933262137,-0.00630171443485821,0.0655530900634018));
#31251=CARTESIAN_POINT('',(-0.00258802439270498,-0.00605955334672256,0.0655236481227066));
#31252=CARTESIAN_POINT('',(-0.00383705340244455,-0.00535659203279485,0.0654598418785206));
#31253=CARTESIAN_POINT('',(-0.00440786581130166,-0.00489679911834568,0.0654270326073568));
#31254=CARTESIAN_POINT('',(-0.0053558302752271,-0.00383705677294902,0.0653647437065981));
#31255=CARTESIAN_POINT('',(-0.00573802192101622,-0.00323921158083279,0.0653350292553776));
#31256=CARTESIAN_POINT('',(-0.00630322602799729,-0.00192008564169453,0.0652709744953718));
#31257=CARTESIAN_POINT('',(-0.0064764665607443,-0.00120850232220196,0.0652382443822136));
#31258=CARTESIAN_POINT('',(-0.0065850576225975,0.000205214722369539,0.0651764815990629));
#31259=CARTESIAN_POINT('',(-0.00652537124758188,0.000915383751165133,0.0651463555003048));
#31260=CARTESIAN_POINT('',(-0.00599520854117729,0.00300392474447296,0.0650499901863294));
#31261=CARTESIAN_POINT('',(-0.00518902617595735,0.00424768704264818,0.064989819431178));
#31262=CARTESIAN_POINT('',(-0.00293340872055775,0.00603025299180784,0.0648610754305156));
#31263=CARTESIAN_POINT('',(-0.00153837411298647,0.0065271503636305,0.0648010896365284));
#31264=CARTESIAN_POINT('',(0.0013372471140284,0.00657130557324581,0.0646722101782343));
#31265=CARTESIAN_POINT('',(0.00274646451239923,0.00611779082991373,0.0646122946360618));
#31266=CARTESIAN_POINT('',(0.00505663061694785,0.00440464740475223,0.0644834016045714));
#31267=CARTESIAN_POINT('',(0.0058999096091617,0.00318752875836041,0.0644234413835539));
#31268=CARTESIAN_POINT('',(0.00669251592029745,0.000423678696913489,0.0642946567060896));
#31269=CARTESIAN_POINT('',(0.00662198505842965,-0.00105646913312049,0.0642345370163344));
#31270=CARTESIAN_POINT('',(0.00583433321739773,-0.00306253721515266,0.0641381209631122));
#31271=CARTESIAN_POINT('',(0.00546807180147761,-0.00367486321330173,0.0641078844342977));
#31272=CARTESIAN_POINT('',(0.00478388959737474,-0.0044880265747629,0.0640616555909692));
#31273=CARTESIAN_POINT('',(0.00453140912573415,-0.00474317143712696,0.0640457796654875));
#31274=CARTESIAN_POINT('',(0.00398596617037514,-0.00520993451354128,0.0640137066350069));
#31275=CARTESIAN_POINT('',(0.00368819903290208,-0.00541317002599699,0.0639975561488288));
#31276=CARTESIAN_POINT('',(0.00339274889905633,-0.00561793598932939,0.0639814493565187));
#31277=CARTESIAN_POINT('',(-0.00687733698154762,0.,0.0668110119055878));
#31278=CARTESIAN_POINT('',(-0.00687733698154762,0.000736490816556296,0.0667811135930194));
#31279=CARTESIAN_POINT('',(-0.00675581752797234,0.00149218713025683,0.066748832740435));
#31280=CARTESIAN_POINT('',(-0.0062712443602323,0.00292218874770557,0.0666843892404749));
#31281=CARTESIAN_POINT('',(-0.00591204429636411,0.00359054047340023,0.0666529431574049));
#31282=CARTESIAN_POINT('',(-0.00501390885293711,0.00476497289265484,0.0665924622051313));
#31283=CARTESIAN_POINT('',(-0.00445681201214791,0.00529189570970565,0.0665600039207699));
#31284=CARTESIAN_POINT('',(-0.00320313581169196,0.00613247539627217,0.0664956213749138));
#31285=CARTESIAN_POINT('',(-0.00251695455175989,0.00644305510131057,0.0664648761206642));
#31286=CARTESIAN_POINT('',(-0.00108514790552801,0.00683157912032622,0.066403759773327));
#31287=CARTESIAN_POINT('',(-0.000321301784850946,0.00691110562198788,0.0663711551720379));
#31288=CARTESIAN_POINT('',(0.00118417239750328,0.00681647647162464,0.0663068943423526));
#31289=CARTESIAN_POINT('',(0.00191358203927076,0.00664753249728436,0.0662767138815832));
#31290=CARTESIAN_POINT('',(0.00329116802672757,0.00608438144295026,0.0662150129357751));
#31291=CARTESIAN_POINT('',(0.00394660878753432,0.00568241328454874,0.0661822936170555));
#31292=CARTESIAN_POINT('',(0.00508338844474566,0.00469304843125292,0.0661182148828016));
#31293=CARTESIAN_POINT('',(0.00555813569912768,0.00411846606696049,0.0660884614837819));
#31294=CARTESIAN_POINT('',(0.00631214164569776,0.0028304598635682,0.0660262284728907));
#31295=CARTESIAN_POINT('',(0.00658810449901086,0.00211210638104738,0.0659934264181678));
#31296=CARTESIAN_POINT('',(0.0068889686223784,0.000637358278077574,0.065929589587556));
#31297=CARTESIAN_POINT('',(0.00691710937426408,-0.00010516963573701,0.0659001242309171));
#31298=CARTESIAN_POINT('',(0.00673270299925258,-0.00159002297834605,0.0658374132868221));
#31299=CARTESIAN_POINT('',(0.00651465405487715,-0.00232843726617145,0.065804560754041));
#31300=CARTESIAN_POINT('',(0.00585817946959136,-0.00368022701192217,0.0657410248797377));
#31301=CARTESIAN_POINT('',(0.00543026833411577,-0.00428627405561341,0.0657117076752329));
#31302=CARTESIAN_POINT('',(0.0043790555373965,-0.00535572890097344,0.0656485743801088));
#31303=CARTESIAN_POINT('',(0.0037566946226163,-0.00580925658295397,0.0656157037963585));
#31304=CARTESIAN_POINT('',(0.00241629697724243,-0.00648241663671485,0.0655525269959273));
#31305=CARTESIAN_POINT('',(0.00170833702218249,-0.00670400649397932,0.0655232176046293));
#31306=CARTESIAN_POINT('',(0.000220716012724379,-0.00691472363109353,0.065459718833647));
#31307=CARTESIAN_POINT('',(-0.000549023210654567,-0.00689610981594638,0.0654268626865835));
#31308=CARTESIAN_POINT('',(-0.0020193534330693,-0.00661664331755768,0.0653641019689896));
#31309=CARTESIAN_POINT('',(-0.00271736120077821,-0.00636238020199629,0.0653346600282944));
#31310=CARTESIAN_POINT('',(-0.00402881057477939,-0.00562428831789364,0.0652708537841083));
#31311=CARTESIAN_POINT('',(-0.00462814939752127,-0.00514151720119214,0.0652380445129446));
#31312=CARTESIAN_POINT('',(-0.00562348849140636,-0.0040288141137252,0.0651757556121858));
#31313=CARTESIAN_POINT('',(-0.00602478020737951,-0.00340109154136163,0.0651460411609653));
#31314=CARTESIAN_POINT('',(-0.00661823045273271,-0.00201604213608617,0.0650819864009596));
#31315=CARTESIAN_POINT('',(-0.00680012870045241,-0.00126889736072759,0.0650492562878014));
#31316=CARTESIAN_POINT('',(-0.00691414661274989,0.000215470351039704,0.0649874935046507));
#31317=CARTESIAN_POINT('',(-0.00685147740447671,0.000961130156365764,0.0649573674058926));
#31318=CARTESIAN_POINT('',(-0.00629481975760744,0.00315404621907631,0.0648610020919172));
#31319=CARTESIAN_POINT('',(-0.00544834833864581,0.00445996567701449,0.0648008313367658));
#31320=CARTESIAN_POINT('',(-0.00308000614899025,0.00633161555857225,0.0646720873361034));
#31321=CARTESIAN_POINT('',(-0.00161525453109883,0.00685334543204856,0.0646121015421161));
#31322=CARTESIAN_POINT('',(0.00140407618790463,0.00689970730319593,0.0644832220838221));
#31323=CARTESIAN_POINT('',(0.00288371938314982,0.00642352810991429,0.0644233065416496));
#31324=CARTESIAN_POINT('',(0.005309336296788,0.00462477015074507,0.0642944135101592));
#31325=CARTESIAN_POINT('',(0.00619475825082075,0.00334682586406391,0.0642344532891416));
#31326=CARTESIAN_POINT('',(0.00702697515087906,0.000444852087110999,0.0641056686116773));
#31327=CARTESIAN_POINT('',(0.00695291950131206,-0.0011092662960417,0.0640455489219221));
#31328=CARTESIAN_POINT('',(0.00612590467155436,-0.00321558785452446,0.0639491328687));
#31329=CARTESIAN_POINT('',(0.00574133930046712,-0.00385851491281968,0.0639188963398855));
#31330=CARTESIAN_POINT('',(0.00502296501430019,-0.00471231620408937,0.063872667496557));
#31331=CARTESIAN_POINT('',(0.00475786680289066,-0.00498021195944635,0.0638567915710753));
#31332=CARTESIAN_POINT('',(0.00418516527491888,-0.00547030157273569,0.0638247185405946));
#31333=CARTESIAN_POINT('',(0.00387251719149399,-0.00568369380262507,0.0638085680544166));
#31334=CARTESIAN_POINT('',(0.00356230190421146,-0.00589869296784463,0.0637924612621064));
#31335=CARTESIAN_POINT('',(-0.00720467396309524,0.,0.0666220238111755));
#31336=CARTESIAN_POINT('',(-0.00720467396309524,0.000771545181563554,0.0665921254986072));
#31337=CARTESIAN_POINT('',(-0.00707737061217141,0.0015632099741909,0.0665598446460228));
#31338=CARTESIAN_POINT('',(-0.00656973347090607,0.00306127462451411,0.0664954011460626));
#31339=CARTESIAN_POINT('',(-0.00619343675102207,0.00376143753484143,0.0664639550629926));
#31340=CARTESIAN_POINT('',(-0.00525255322852593,0.00499176879461846,0.066403474110719));
#31341=CARTESIAN_POINT('',(-0.00466894054319066,0.00554377127911973,0.0663710158263576));
#31342=CARTESIAN_POINT('',(-0.00335559377774765,0.00642435959374813,0.0663066332805016));
#31343=CARTESIAN_POINT('',(-0.00263675271024423,0.00674972179722307,0.066275888026252));
#31344=CARTESIAN_POINT('',(-0.00113679711813476,0.00715673818908369,0.0662147716789148));
#31345=CARTESIAN_POINT('',(-0.000336594616466026,0.00724004987170665,0.0661821670776257));
#31346=CARTESIAN_POINT('',(0.00124053482663403,0.00714091670757624,0.0661179062479404));
#31347=CARTESIAN_POINT('',(0.00200466179446659,0.00696393159598188,0.066087725787171));
#31348=CARTESIAN_POINT('',(0.00344781601569853,0.00637397653789229,0.0660260248413628));
#31349=CARTESIAN_POINT('',(0.00413445344475077,0.00595287611303322,0.0659933055226432));
#31350=CARTESIAN_POINT('',(0.00532533980382573,0.00491642098255655,0.0659292267883894));
#31351=CARTESIAN_POINT('',(0.00582268335291664,0.00431449052447686,0.0658994733893697));
#31352=CARTESIAN_POINT('',(0.00661257732290065,0.00296517976905168,0.0658372403784784));
#31353=CARTESIAN_POINT('',(0.00690167503461391,0.00221263519464696,0.0658044383237555));
#31354=CARTESIAN_POINT('',(0.0072168592290007,0.000667694283928396,0.0657406014931437));
#31355=CARTESIAN_POINT('',(0.00724633938141386,-0.000110175339427985,0.0657111361365049));
#31356=CARTESIAN_POINT('',(0.00705315591341762,-0.0016657024635479,0.0656484251924099));
#31357=CARTESIAN_POINT('',(0.00682472860842485,-0.00243926266682821,0.0656155726596287));
#31358=CARTESIAN_POINT('',(0.00613700814849502,-0.00385539283624122,0.0655520367853255));
#31359=CARTESIAN_POINT('',(0.00568872995236311,-0.00449028558147216,0.0655227195808207));
#31360=CARTESIAN_POINT('',(0.00458748313451537,-0.00561064270512987,0.0654595862856965));
#31361=CARTESIAN_POINT('',(0.00393550003547636,-0.00608575670502184,0.0654267157019463));
#31362=CARTESIAN_POINT('',(0.00253130419023423,-0.00679095680287067,0.0653635389015151));
#31363=CARTESIAN_POINT('',(0.00178964783853592,-0.00702309355571597,0.0653342295102171));
#31364=CARTESIAN_POINT('',(0.000231221316387449,-0.00724384008528374,0.0652707307392347));
#31365=CARTESIAN_POINT('',(-0.000575154778884747,-0.00722434031819303,0.0652378745921713));
#31366=CARTESIAN_POINT('',(-0.00211546753351723,-0.00693157220025716,0.0651751138745773));
#31367=CARTESIAN_POINT('',(-0.00284669800885144,-0.00666520705727002,0.0651456719338822));
#31368=CARTESIAN_POINT('',(-0.00422056774711423,-0.00589198460299243,0.0650818656896961));
#31369=CARTESIAN_POINT('',(-0.00484843298374087,-0.0053862352840386,0.0650490564185323));
#31370=CARTESIAN_POINT('',(-0.00589114670758562,-0.00422057145450138,0.0649867675177736));
#31371=CARTESIAN_POINT('',(-0.00631153849374279,-0.00356297150189047,0.0649570530665531));
#31372=CARTESIAN_POINT('',(-0.00693323487746813,-0.0021119986304778,0.0648929983065474));
#31373=CARTESIAN_POINT('',(-0.00712379084016052,-0.00132929239925322,0.0648602681933891));
#31374=CARTESIAN_POINT('',(-0.00724323560290229,0.000225725979709869,0.0647985054102385));
#31375=CARTESIAN_POINT('',(-0.00717758356137153,0.0010068765615664,0.0647683793114804));
#31376=CARTESIAN_POINT('',(-0.00659443097403759,0.00330416769367967,0.0646720139975049));
#31377=CARTESIAN_POINT('',(-0.00570767050133428,0.00467224431138081,0.0646118432423536));
#31378=CARTESIAN_POINT('',(-0.00322660357742274,0.00663297812533666,0.0644830992416911));
#31379=CARTESIAN_POINT('',(-0.0016921349492112,0.00717954050046661,0.0644231134477039));
#31380=CARTESIAN_POINT('',(0.00147090526178086,0.00722810903314606,0.0642942339894098));
#31381=CARTESIAN_POINT('',(0.00302097425390042,0.00672926538991485,0.0642343184472374));
#31382=CARTESIAN_POINT('',(0.00556204197662814,0.00484489289673792,0.064105425415747));
#31383=CARTESIAN_POINT('',(0.00648960689247979,0.00350612296976741,0.0640454651947294));
#31384=CARTESIAN_POINT('',(0.00736143438146067,0.000466025477308509,0.0639166805172651));
#31385=CARTESIAN_POINT('',(0.00728385394419447,-0.00116206345896291,0.0638565608275099));
#31386=CARTESIAN_POINT('',(0.006417476125711,-0.00336863849389627,0.0637601447742877));
#31387=CARTESIAN_POINT('',(0.00601460679945664,-0.00404216661233763,0.0637299082454732));
#31388=CARTESIAN_POINT('',(0.00526204043122564,-0.00493660583341584,0.0636836794021448));
#31389=CARTESIAN_POINT('',(0.00498432448004717,-0.00521725248176574,0.0636678034766631));
#31390=CARTESIAN_POINT('',(0.00438436437946263,-0.00573066863193009,0.0636357304461824));
#31391=CARTESIAN_POINT('',(0.0040568353500859,-0.00595421757925314,0.0636195799600043));
#31392=CARTESIAN_POINT('',(0.00373185490936659,-0.00617944994635986,0.0636034731676942));
#31393=CARTESIAN_POINT('',(-0.00753201094464286,0.,0.0664330357167633));
#31394=CARTESIAN_POINT('',(-0.00753201094464286,0.000806599546570811,0.0664031374041949));
#31395=CARTESIAN_POINT('',(-0.00739892369637049,0.00163423281812497,0.0663708565516105));
#31396=CARTESIAN_POINT('',(-0.00686822258157983,0.00320036050132265,0.0663064130516504));
#31397=CARTESIAN_POINT('',(-0.00647482920568002,0.00393233459628263,0.0662749669685803));
#31398=CARTESIAN_POINT('',(-0.00549119760411474,0.00521856469658208,0.0662144860163068));
#31399=CARTESIAN_POINT('',(-0.0048810690742334,0.00579564684853382,0.0661820277319454));
#31400=CARTESIAN_POINT('',(-0.00350805174380334,0.00671624379122409,0.0661176451860894));
#31401=CARTESIAN_POINT('',(-0.00275655086872857,0.00705638849313556,0.0660868999318397));
#31402=CARTESIAN_POINT('',(-0.00118844633074152,0.00748189725784116,0.0660257835845025));
#31403=CARTESIAN_POINT('',(-0.000351887448081106,0.00756899412142541,0.0659931789832135));
#31404=CARTESIAN_POINT('',(0.00129689725576478,0.00746535694352784,0.0659289181535282));
#31405=CARTESIAN_POINT('',(0.00209574154966243,0.0072803306946794,0.0658987376927588));
#31406=CARTESIAN_POINT('',(0.00360446400466949,0.00666357163283433,0.0658370367469506));
#31407=CARTESIAN_POINT('',(0.00432229810196721,0.0062233389415177,0.065804317428231));
#31408=CARTESIAN_POINT('',(0.0055672911629058,0.00513979353386018,0.0657402386939771));
#31409=CARTESIAN_POINT('',(0.00608723100670561,0.00451051498199323,0.0657104852949574));
#31410=CARTESIAN_POINT('',(0.00691301300010353,0.00309989967453515,0.0656482522840662));
#31411=CARTESIAN_POINT('',(0.00721524557021695,0.00231316400824654,0.0656154502293433));
#31412=CARTESIAN_POINT('',(0.007544749835623,0.000698030289779218,0.0655516133987315));
#31413=CARTESIAN_POINT('',(0.00757556938856363,-0.000115181043118961,0.0655221480420927));
#31414=CARTESIAN_POINT('',(0.00737360882758266,-0.00174138194874975,0.0654594370979977));
#31415=CARTESIAN_POINT('',(0.00713480316197254,-0.00255008806748497,0.0654265845652165));
#31416=CARTESIAN_POINT('',(0.00641583682739869,-0.00403055866056026,0.0653630486909132));
#31417=CARTESIAN_POINT('',(0.00594719157061045,-0.00469429710733092,0.0653337314864085));
#31418=CARTESIAN_POINT('',(0.00479591073163425,-0.0058655565092863,0.0652705981912843));
#31419=CARTESIAN_POINT('',(0.00411430544833643,-0.00636225682708971,0.065237727607534));
#31420=CARTESIAN_POINT('',(0.00264631140322602,-0.0070994969690265,0.0651745508071028));
#31421=CARTESIAN_POINT('',(0.00187095865488935,-0.00734218061745262,0.0651452414158048));
#31422=CARTESIAN_POINT('',(0.00024172662005052,-0.00757295653947395,0.0650817426448225));
#31423=CARTESIAN_POINT('',(-0.000601286347114926,-0.00755257082043967,0.065048886497759));
#31424=CARTESIAN_POINT('',(-0.00221158163396516,-0.00724650108295663,0.0649861257801651));
#31425=CARTESIAN_POINT('',(-0.00297603481692467,-0.00696803391254375,0.06495668383947));
#31426=CARTESIAN_POINT('',(-0.00441232491944907,-0.00615968088809122,0.0648928775952838));
#31427=CARTESIAN_POINT('',(-0.00506871656996048,-0.00563095336688506,0.0648600683241201));
#31428=CARTESIAN_POINT('',(-0.00615880492376489,-0.00441232879527757,0.0647977794233614));
#31429=CARTESIAN_POINT('',(-0.00659829678010608,-0.00372485146241931,0.0647680649721409));
#31430=CARTESIAN_POINT('',(-0.00724823930220355,-0.00220795512486944,0.0647040102121351));
#31431=CARTESIAN_POINT('',(-0.00744745297986863,-0.00138968743777885,0.0646712800989769));
#31432=CARTESIAN_POINT('',(-0.00757232459305469,0.000235981608380033,0.0646095173158262));
#31433=CARTESIAN_POINT('',(-0.00750368971826635,0.00105262296676703,0.0645793912170681));
#31434=CARTESIAN_POINT('',(-0.00689404219046773,0.00345428916828302,0.0644830259030927));
#31435=CARTESIAN_POINT('',(-0.00596699266402274,0.00488452294574713,0.0644228551479413));
#31436=CARTESIAN_POINT('',(-0.00337320100585524,0.00693434069210107,0.0642941111472789));
#31437=CARTESIAN_POINT('',(-0.00176901536732356,0.00750573556888466,0.0642341253532916));
#31438=CARTESIAN_POINT('',(0.0015377343356571,0.00755651076309619,0.0641052458949976));
#31439=CARTESIAN_POINT('',(0.00315822912465102,0.00703500266991541,0.0640453303528252));
#31440=CARTESIAN_POINT('',(0.00581474765646829,0.00506501564273076,0.0639164373213348));
#31441=CARTESIAN_POINT('',(0.00678445553413884,0.00366542007547091,0.0638564771003172));
#31442=CARTESIAN_POINT('',(0.00769589361204228,0.00048719886750602,0.0637276924228528));
#31443=CARTESIAN_POINT('',(0.00761478838707688,-0.00121486062188411,0.0636675727330976));
#31444=CARTESIAN_POINT('',(0.00670904757986764,-0.00352168913326807,0.0635711566798755));
#31445=CARTESIAN_POINT('',(0.00628787429844615,-0.00422581831185558,0.063540920151061));
#31446=CARTESIAN_POINT('',(0.00550111584815108,-0.00516089546274231,0.0634946913077325));
#31447=CARTESIAN_POINT('',(0.00521078215720368,-0.00545429300408513,0.0634788153822508));
#31448=CARTESIAN_POINT('',(0.00458356348400637,-0.0059910356911245,0.0634467423517701));
#31449=CARTESIAN_POINT('',(0.00424115350867781,-0.00622474135588122,0.0634305918655921));
#31450=CARTESIAN_POINT('',(0.00390140791452173,-0.0064602069248751,0.0634144850732819));
#31451=CARTESIAN_POINT('',(-0.00704100547232143,0.,0.0667165178583817));
#31452=CARTESIAN_POINT('',(-0.00655,0.,0.067));
#31453=CARTESIAN_POINT('',(-0.00753201094464286,0.,0.0664330357167633));
#31454=CARTESIAN_POINT('',(-0.00753201094464286,0.,0.0664330357167633));
#31455=CARTESIAN_POINT('',(-0.00753201094464286,0.00244729870815628,0.066342321431049));
#31456=CARTESIAN_POINT('',(-0.00609352485603417,0.00442720495336657,0.0662516071453347));
#31457=CARTESIAN_POINT('',(-0.00465503876742549,0.00640711119857685,0.0661608928596204));
#31458=CARTESIAN_POINT('',(-0.00232751938371274,0.00716336808970901,0.0660701785739062));
#31459=CARTESIAN_POINT('',(-4.84937169161726E-19,0.00791962498084115,0.0659794642881919));
#31460=CARTESIAN_POINT('',(0.00232751938371274,0.00716336808970901,0.0658887500024776));
#31461=CARTESIAN_POINT('',(0.00465503876742549,0.00640711119857685,0.0657980357167633));
#31462=CARTESIAN_POINT('',(0.00609352485603417,0.00442720495336657,0.065707321431049));
#31463=CARTESIAN_POINT('',(0.00753201094464286,0.00244729870815628,0.0656166071453347));
#31464=CARTESIAN_POINT('',(0.00753201094464286,9.22405309449971E-19,0.0655258928596205));
#31465=CARTESIAN_POINT('',(0.00753201094464286,-0.00244729870815628,0.0654351785739062));
#31466=CARTESIAN_POINT('',(0.00609352485603417,-0.00442720495336657,0.0653444642881919));
#31467=CARTESIAN_POINT('',(0.00465503876742549,-0.00640711119857685,0.0652537500024776));
#31468=CARTESIAN_POINT('',(0.00232751938371274,-0.00716336808970901,0.0651630357167633));
#31469=CARTESIAN_POINT('',(1.45481150748518E-18,-0.00791962498084115,0.0650723214310489));
#31470=CARTESIAN_POINT('',(-0.00232751938371274,-0.00716336808970901,0.0649816071453347));
#31471=CARTESIAN_POINT('',(-0.00465503876742549,-0.00640711119857685,0.0648908928596204));
#31472=CARTESIAN_POINT('',(-0.00609352485603417,-0.00442720495336658,0.0648001785739062));
#31473=CARTESIAN_POINT('',(-0.00753201094464286,-0.00244729870815628,0.0647094642881918));
#31474=CARTESIAN_POINT('',(-0.00753201094464286,0.,0.0646187500024776));
#31475=CARTESIAN_POINT('',(-0.00753201094464286,0.00244729870815628,0.0645280357167632));
#31476=CARTESIAN_POINT('',(-0.00609352485603417,0.00442720495336657,0.064437321431049));
#31477=CARTESIAN_POINT('',(-0.00465503876742549,0.00640711119857685,0.0643466071453347));
#31478=CARTESIAN_POINT('',(-0.00232751938371274,0.00716336808970901,0.0642558928596204));
#31479=CARTESIAN_POINT('',(-4.84937169161726E-19,0.00791962498084115,0.0641651785739061));
#31480=CARTESIAN_POINT('',(0.00232751938371274,0.00716336808970901,0.0640744642881919));
#31481=CARTESIAN_POINT('',(0.00465503876742549,0.00640711119857685,0.0639837500024776));
#31482=CARTESIAN_POINT('',(0.00609352485603417,0.00442720495336657,0.0638930357167633));
#31483=CARTESIAN_POINT('',(0.00753201094464286,0.00244729870815628,0.063802321431049));
#31484=CARTESIAN_POINT('',(0.00753201094464286,9.22405309449971E-19,0.0637116071453347));
#31485=CARTESIAN_POINT('',(0.00753201094464286,-0.00244729870815628,0.0636208928596204));
#31486=CARTESIAN_POINT('',(0.00609352485603417,-0.00442720495336657,0.0635301785739062));
#31487=CARTESIAN_POINT('',(0.00534171654646512,-0.00546198031831741,0.0634827677895151));
#31488=CARTESIAN_POINT('',(0.00429046182728509,-0.00619056751670065,0.0634329294936898));
#31489=CARTESIAN_POINT('',(0.00429046182728508,-0.00619056751670066,0.0634329294936898));
#31490=CARTESIAN_POINT('',(0.00401076826589901,-0.00578701097100319,0.063716411528697));
#31491=CARTESIAN_POINT('',(0.00373107470451293,-0.00538345442530572,0.0639998935637042));
#31492=CARTESIAN_POINT('',(0.00655,8.02143653441517E-19,0.0642785714285715));
#31493=CARTESIAN_POINT('',(0.00655000000000002,-0.00212822401032552,0.0641878571428572));
#31494=CARTESIAN_POINT('',(0.00529906131315591,-0.0038499934025157,0.0640971428571429));
#31495=CARTESIAN_POINT('',(0.00464527107021772,-0.00474985847267627,0.0640497319684088));
#31496=CARTESIAN_POINT('',(0.00373107470451293,-0.00538345442530572,0.0639998935637043));
#31497=CARTESIAN_POINT('',(0.00655,8.02143653441516E-19,0.0642785714285715));
#31498=CARTESIAN_POINT('',(-0.00655,0.,0.0651857142857143));
#31499=CARTESIAN_POINT('',(-0.00655000000000001,0.00212822401032553,0.065095));
#31500=CARTESIAN_POINT('',(-0.00529906131315591,0.0038499934025157,0.0650042857142857));
#31501=CARTESIAN_POINT('',(-0.00404812262631181,0.00557176279470586,0.0649135714285714));
#31502=CARTESIAN_POINT('',(-0.0020240613131559,0.00622942018173326,0.0648228571428572));
#31503=CARTESIAN_POINT('',(-4.21711875003113E-19,0.00688707756876065,0.0647321428571428));
#31504=CARTESIAN_POINT('',(0.0020240613131559,0.00622942018173326,0.0646414285714286));
#31505=CARTESIAN_POINT('',(0.00404812262631181,0.00557176279470586,0.0645507142857142));
#31506=CARTESIAN_POINT('',(0.00529906131315591,0.0038499934025157,0.06446));
#31507=CARTESIAN_POINT('',(0.00654999999999999,0.00212822401032556,0.0643692857142857));
#31508=CARTESIAN_POINT('',(0.00655,8.02143653441516E-19,0.0642785714285714));
#31509=CARTESIAN_POINT('',(-0.00655,0.,0.0651857142857143));
#31510=CARTESIAN_POINT('',(0.00655,8.02143653441517E-19,0.0660928571428572));
#31511=CARTESIAN_POINT('',(0.00655000000000001,-0.00212822401032553,0.0660021428571429));
#31512=CARTESIAN_POINT('',(0.00529906131315591,-0.0038499934025157,0.0659114285714286));
#31513=CARTESIAN_POINT('',(0.00404812262631181,-0.00557176279470586,0.0658207142857143));
#31514=CARTESIAN_POINT('',(0.0020240613131559,-0.00622942018173326,0.06573));
#31515=CARTESIAN_POINT('',(1.26513562500934E-18,-0.00688707756876065,0.0656392857142857));
#31516=CARTESIAN_POINT('',(-0.0020240613131559,-0.00622942018173326,0.0655485714285714));
#31517=CARTESIAN_POINT('',(-0.00404812262631181,-0.00557176279470586,0.0654578571428572));
#31518=CARTESIAN_POINT('',(-0.00529906131315591,-0.0038499934025157,0.0653671428571429));
#31519=CARTESIAN_POINT('',(-0.00654999999999999,-0.00212822401032555,0.0652764285714286));
#31520=CARTESIAN_POINT('',(-0.00655,0.,0.0651857142857143));
#31521=CARTESIAN_POINT('',(0.00655,8.02143653441516E-19,0.0660928571428572));
#31522=CARTESIAN_POINT('',(-0.00655,0.,0.067));
#31523=CARTESIAN_POINT('',(-0.00655,0.00212822401032553,0.0669092857142857));
#31524=CARTESIAN_POINT('',(-0.00529906131315591,0.0038499934025157,0.0668185714285715));
#31525=CARTESIAN_POINT('',(-0.00404812262631181,0.00557176279470586,0.0667278571428571));
#31526=CARTESIAN_POINT('',(-0.0020240613131559,0.00622942018173326,0.0666371428571429));
#31527=CARTESIAN_POINT('',(-4.21711875003113E-19,0.00688707756876065,0.0665464285714285));
#31528=CARTESIAN_POINT('',(0.0020240613131559,0.00622942018173326,0.0664557142857143));
#31529=CARTESIAN_POINT('',(0.00404812262631181,0.00557176279470586,0.066365));
#31530=CARTESIAN_POINT('',(0.00529906131315591,0.0038499934025157,0.0662742857142857));
#31531=CARTESIAN_POINT('',(0.00654999999999999,0.00212822401032555,0.0661835714285715));
#31532=CARTESIAN_POINT('',(0.00655,8.02143653441516E-19,0.0660928571428572));
#31533=CARTESIAN_POINT('',(-3.90312782094781E-18,0.,0.0657884338054059));
#31534=CARTESIAN_POINT('',(-0.00753201094464286,0.,0.0663196428596204));
#31535=CARTESIAN_POINT('',(0.00429046128025484,-0.00619056789582776,0.0633195366106131));
#31536=CARTESIAN_POINT('',(0.0042904607332246,-0.00619056827495487,0.0632628401561078));
#31537=CARTESIAN_POINT('',(0.00373107721004495,-0.00538345487953476,0.0639998935637042));
#31538=CARTESIAN_POINT('',(-0.00753201094464286,0.,0.0663196428596204));
#31539=CARTESIAN_POINT('',(-0.00655,0.,0.0663196428596204));
#31540=CARTESIAN_POINT('',(0.,0.,0.062));
#31541=CARTESIAN_POINT('',(0.,0.,0.062));
#31542=CARTESIAN_POINT('',(0.00655,0.,0.062));
#31543=CARTESIAN_POINT('',(0.,0.,0.062));
#31544=CARTESIAN_POINT('',(0.00855,0.,0.062));
#31545=CARTESIAN_POINT('',(0.,0.,0.064));
#31546=CARTESIAN_POINT('',(-0.025980762113538,-0.0149999999999972,0.064));
#31547=CARTESIAN_POINT('',(-0.028759522113538,-0.0149999999999972,0.064));
#31548=CARTESIAN_POINT('',(0.0259807621135283,-0.0150000000000028,0.064));
#31549=CARTESIAN_POINT('',(0.0232020021135283,-0.0150000000000028,0.064));
#31550=CARTESIAN_POINT('',(0.,0.03,0.064));
#31551=CARTESIAN_POINT('',(-0.00277876,0.03,0.064));
#31552=CARTESIAN_POINT('',(-0.0259807621135331,-0.015,0.064));
#31553=CARTESIAN_POINT('',(0.,0.,0.064));
#31554=CARTESIAN_POINT('',(-0.01055,0.,0.064));
#31555=CARTESIAN_POINT('',(0.,0.,0.064));
#31556=CARTESIAN_POINT('',(-0.00493432083723898,0.00759818777748466,0.064));
#31557=CARTESIAN_POINT('',(-0.0259807621135331,-0.015,0.064));
#31558=CARTESIAN_POINT('',(-0.0259807621135331,-0.015,0.065));
#31559=CARTESIAN_POINT('',(-0.0259807621135331,-0.015,0.066));
#31560=CARTESIAN_POINT('',(0.00411306321940664,-0.00807234108421418,0.064));
#31561=CARTESIAN_POINT('',(-0.00356046479940298,-0.0119821988972063,0.064));
#31562=CARTESIAN_POINT('',(0.,0.,0.064));
#31563=CARTESIAN_POINT('',(-0.00411306321940666,-0.00807234108421419,0.064));
#31564=CARTESIAN_POINT('',(0.00493432083723899,0.00759818777748466,0.064));
#31565=CARTESIAN_POINT('',(0.,0.,0.064));
#31566=CARTESIAN_POINT('',(0.00904738405664563,0.000474153306729528,0.064));
#31567=CARTESIAN_POINT('',(0.,0.03,0.064));
#31568=CARTESIAN_POINT('',(-0.00904738405664563,0.000474153306729528,0.064));
#31569=CARTESIAN_POINT('',(0.,0.,0.067));
#31570=CARTESIAN_POINT('',(-0.0259807621135331,-0.015,0.067));
#31571=CARTESIAN_POINT('',(0.,0.03,0.067));
#31572=CARTESIAN_POINT('',(-0.0012192,0.03,0.067));
#31573=CARTESIAN_POINT('',(0.0259807621135283,-0.0150000000000028,0.067));
#31574=CARTESIAN_POINT('',(0.0247615621135283,-0.0150000000000028,0.067));
#31575=CARTESIAN_POINT('',(-0.025980762113538,-0.0149999999999972,0.067));
#31576=CARTESIAN_POINT('',(-0.027199962113538,-0.0149999999999972,0.067));
#31577=CARTESIAN_POINT('',(0.,0.,0.067));
#31578=CARTESIAN_POINT('',(0.,0.,0.064));
#31579=CARTESIAN_POINT('',(0.0259807621135331,-0.015,0.064));
#31580=CARTESIAN_POINT('',(-0.025980762113538,-0.0149999999999972,0.064));
#31581=CARTESIAN_POINT('',(-0.025980762113538,-0.0149999999999972,0.064));
#31582=CARTESIAN_POINT('',(0.0259807621135283,-0.0150000000000028,0.064));
#31583=CARTESIAN_POINT('',(0.0259807621135283,-0.0150000000000028,0.064));
#31584=CARTESIAN_POINT('',(0.,0.03,0.064));
#31585=CARTESIAN_POINT('',(0.,0.03,0.064));
#31586=CARTESIAN_POINT('',(-0.0259807621135331,-0.015,0.066));
#31587=CARTESIAN_POINT('',(-0.0259807621135331,-0.015,0.065));
#31588=CARTESIAN_POINT('',(0.,0.,0.063));
#31589=CARTESIAN_POINT('',(0.,0.,0.063));
#31590=CARTESIAN_POINT('',(-0.00955,0.,0.063));
#31591=CARTESIAN_POINT('',(0.,0.,0.063));
#45463=MECHANICAL_DESIGN_GEOMETRIC_PRESENTATION_REPRESENTATION('',(#13534),#45464);
#45464=(
GEOMETRIC_REPRESENTATION_CONTEXT(3)
GLOBAL_UNCERTAINTY_ASSIGNED_CONTEXT((#45492))
GLOBAL_UNIT_ASSIGNED_CONTEXT((#45522,#45521,#45520))
REPRESENTATION_CONTEXT('MAS-690','TOP_LEVEL_ASSEMBLY_PART')
);
#45470=(
GEOMETRIC_REPRESENTATION_CONTEXT(3)
GLOBAL_UNCERTAINTY_ASSIGNED_CONTEXT((#45498))
GLOBAL_UNIT_ASSIGNED_CONTEXT((#45522,#45521,#45520))
REPRESENTATION_CONTEXT('floating_ring_bottom_connector',
'COMPONENT_PART')
);
#45492=UNCERTAINTY_MEASURE_WITH_UNIT(LENGTH_MEASURE(1.E-8),#45522,
'DISTANCE_ACCURACY_VALUE','Maximum Tolerance applied to model');
#45498=UNCERTAINTY_MEASURE_WITH_UNIT(LENGTH_MEASURE(2.E-5),#45522,
'DISTANCE_ACCURACY_VALUE','Maximum Tolerance applied to model');
#45520=(
NAMED_UNIT(*)
SI_UNIT($,.STERADIAN.)
SOLID_ANGLE_UNIT()
);
#45521=(
NAMED_UNIT(*)
PLANE_ANGLE_UNIT()
SI_UNIT($,.RADIAN.)
);
#45522=(
LENGTH_UNIT()
NAMED_UNIT(*)
SI_UNIT($,.METRE.)
);
#45534=PRODUCT_DEFINITION_SHAPE('','',#45591);
#45591=PRODUCT_DEFINITION('','',#45647,#45619);
#45619=PRODUCT_DEFINITION_CONTEXT('',#45782,'design');
#45647=PRODUCT_DEFINITION_FORMATION_WITH_SPECIFIED_SOURCE('','',#45703,
 .NOT_KNOWN.);
#45703=PRODUCT('floating_ring_bottom_connector',
'floating_ring_bottom_connector','floating_ring_bottom_connector',(#45759));
#45759=PRODUCT_CONTEXT('',#45782,'mechanical');
#45782=APPLICATION_CONTEXT('managed model based 3d engineering');
ENDSEC;
END-ISO-10303-21;
